ISO-10303-21;
HEADER;
/* Generated by software containing ST-Developer
 * from STEP Tools, Inc. (www.steptools.com) 
 */

FILE_DESCRIPTION(
/* description */ (''),
/* implementation_level */ '2;1');

FILE_NAME(
/* name */ 'ISO 10642 - M2 x 4 - 10.9 (Pointer Screw).step',
/* time_stamp */ '2026-10-05T09:57:53+05:00',
/* author */ (''),
/* organization */ (''),
/* preprocessor_version */ 'ST-DEVELOPER v20.2',
/* originating_system */ 'Autodesk Translation Framework v15.15.0.0',
/* authorisation */ '');

FILE_SCHEMA (('AUTOMOTIVE_DESIGN { 1 0 10303 214 3 1 1 }'));
ENDSEC;

DATA;
#10=MECHANICAL_DESIGN_GEOMETRIC_PRESENTATION_REPRESENTATION('',(#566),#113984);
#530=SHAPE_REPRESENTATION_RELATIONSHIP('SRR','None',#114067,#548);
#548=ADVANCED_BREP_SHAPE_REPRESENTATION('',(#584),#113981);
#566=STYLED_ITEM('',(#114317),#584);
#584=MANIFOLD_SOLID_BREP('ISO 10642 - M2 x 4 - 10.9 (Pointer Screw)',#60407);
#823=CYLINDRICAL_SURFACE('',#63422,0.96675);
#824=CYLINDRICAL_SURFACE('',#63424,0.96675);
#825=CYLINDRICAL_SURFACE('',#63425,0.96675);
#826=CYLINDRICAL_SURFACE('',#63426,0.96675);
#827=CYLINDRICAL_SURFACE('',#63427,0.96675);
#828=CYLINDRICAL_SURFACE('',#63428,0.96675);
#829=CYLINDRICAL_SURFACE('',#63429,0.96675);
#830=CYLINDRICAL_SURFACE('',#63430,0.96675);
#831=CYLINDRICAL_SURFACE('',#63432,0.739000000000001);
#832=CYLINDRICAL_SURFACE('',#63434,0.739000000000001);
#833=CYLINDRICAL_SURFACE('',#63435,0.739000000000001);
#834=CYLINDRICAL_SURFACE('',#63436,0.739000000000001);
#835=CYLINDRICAL_SURFACE('',#63437,0.739000000000001);
#836=CYLINDRICAL_SURFACE('',#63438,0.739000000000001);
#837=CYLINDRICAL_SURFACE('',#63439,0.739000000000001);
#838=CYLINDRICAL_SURFACE('',#63446,0.739000000000001);
#839=CYLINDRICAL_SURFACE('',#63457,0.96675);
#949=CONICAL_SURFACE('',#63456,0.899999999999999,0.785398163397426);
#950=CONICAL_SURFACE('',#63459,1.45,0.785398163397448);
#1420=CIRCLE('',#63423,0.96675);
#1421=CIRCLE('',#63431,0.96675);
#1422=CIRCLE('',#63433,0.739000000000001);
#1423=CIRCLE('',#63441,0.96675);
#1424=CIRCLE('',#63443,0.96675);
#1425=CIRCLE('',#63444,0.96675);
#1426=CIRCLE('',#63445,0.739000000000001);
#1427=CIRCLE('',#63455,0.800000000000001);
#1428=CIRCLE('',#63458,0.96675);
#1429=CIRCLE('',#63460,1.9);
#1856=FACE_BOUND('',#10695,.T.);
#3881=PLANE('',#63440);
#3882=PLANE('',#63442);
#3883=PLANE('',#63447);
#3884=PLANE('',#63448);
#3885=PLANE('',#63449);
#3886=PLANE('',#63450);
#3887=PLANE('',#63451);
#3888=PLANE('',#63452);
#3889=PLANE('',#63453);
#3890=PLANE('',#63454);
#3891=PLANE('',#63461);
#7082=FACE_OUTER_BOUND('',#10663,.T.);
#7083=FACE_OUTER_BOUND('',#10664,.T.);
#7084=FACE_OUTER_BOUND('',#10665,.T.);
#7085=FACE_OUTER_BOUND('',#10666,.T.);
#7086=FACE_OUTER_BOUND('',#10667,.T.);
#7087=FACE_OUTER_BOUND('',#10668,.T.);
#7088=FACE_OUTER_BOUND('',#10669,.T.);
#7089=FACE_OUTER_BOUND('',#10670,.T.);
#7090=FACE_OUTER_BOUND('',#10671,.T.);
#7091=FACE_OUTER_BOUND('',#10672,.T.);
#7092=FACE_OUTER_BOUND('',#10673,.T.);
#7093=FACE_OUTER_BOUND('',#10674,.T.);
#7094=FACE_OUTER_BOUND('',#10675,.T.);
#7095=FACE_OUTER_BOUND('',#10676,.T.);
#7096=FACE_OUTER_BOUND('',#10677,.T.);
#7097=FACE_OUTER_BOUND('',#10678,.T.);
#7098=FACE_OUTER_BOUND('',#10679,.T.);
#7099=FACE_OUTER_BOUND('',#10680,.T.);
#7100=FACE_OUTER_BOUND('',#10681,.T.);
#7101=FACE_OUTER_BOUND('',#10682,.T.);
#7102=FACE_OUTER_BOUND('',#10683,.T.);
#7103=FACE_OUTER_BOUND('',#10684,.T.);
#7104=FACE_OUTER_BOUND('',#10685,.T.);
#7105=FACE_OUTER_BOUND('',#10686,.T.);
#7106=FACE_OUTER_BOUND('',#10687,.T.);
#7107=FACE_OUTER_BOUND('',#10688,.T.);
#7108=FACE_OUTER_BOUND('',#10689,.T.);
#7109=FACE_OUTER_BOUND('',#10690,.T.);
#7110=FACE_OUTER_BOUND('',#10691,.T.);
#7111=FACE_OUTER_BOUND('',#10692,.T.);
#7112=FACE_OUTER_BOUND('',#10693,.T.);
#7113=FACE_OUTER_BOUND('',#10694,.T.);
#10663=EDGE_LOOP('',(#55255,#55256,#55257,#55258));
#10664=EDGE_LOOP('',(#55259,#55260,#55261,#55262));
#10665=EDGE_LOOP('',(#55263,#55264,#55265,#55266));
#10666=EDGE_LOOP('',(#55267,#55268,#55269,#55270));
#10667=EDGE_LOOP('',(#55271,#55272,#55273,#55274));
#10668=EDGE_LOOP('',(#55275,#55276,#55277,#55278));
#10669=EDGE_LOOP('',(#55279,#55280,#55281,#55282));
#10670=EDGE_LOOP('',(#55283,#55284,#55285,#55286,#55287));
#10671=EDGE_LOOP('',(#55288,#55289,#55290,#55291));
#10672=EDGE_LOOP('',(#55292,#55293,#55294,#55295));
#10673=EDGE_LOOP('',(#55296,#55297,#55298,#55299));
#10674=EDGE_LOOP('',(#55300,#55301,#55302,#55303));
#10675=EDGE_LOOP('',(#55304,#55305,#55306,#55307));
#10676=EDGE_LOOP('',(#55308,#55309,#55310,#55311));
#10677=EDGE_LOOP('',(#55312,#55313,#55314,#55315));
#10678=EDGE_LOOP('',(#55316,#55317,#55318,#55319));
#10679=EDGE_LOOP('',(#55320,#55321,#55322,#55323,#55324,#55325,#55326,#55327,
#55328,#55329,#55330,#55331,#55332,#55333,#55334,#55335,#55336,#55337,#55338));
#10680=EDGE_LOOP('',(#55339,#55340,#55341,#55342,#55343));
#10681=EDGE_LOOP('',(#55344,#55345,#55346,#55347));
#10682=EDGE_LOOP('',(#55348,#55349,#55350,#55351,#55352,#55353,#55354,#55355,
#55356,#55357,#55358,#55359,#55360,#55361,#55362,#55363,#55364,#55365));
#10683=EDGE_LOOP('',(#55366,#55367,#55368,#55369));
#10684=EDGE_LOOP('',(#55370,#55371,#55372,#55373));
#10685=EDGE_LOOP('',(#55374,#55375,#55376,#55377));
#10686=EDGE_LOOP('',(#55378,#55379,#55380,#55381));
#10687=EDGE_LOOP('',(#55382,#55383,#55384,#55385));
#10688=EDGE_LOOP('',(#55386,#55387,#55388,#55389));
#10689=EDGE_LOOP('',(#55390,#55391,#55392,#55393,#55394,#55395));
#10690=EDGE_LOOP('',(#55396));
#10691=EDGE_LOOP('',(#55397,#55398,#55399,#55400,#55401,#55402));
#10692=EDGE_LOOP('',(#55403,#55404,#55405));
#10693=EDGE_LOOP('',(#55406,#55407,#55408,#55409,#55410,#55411));
#10694=EDGE_LOOP('',(#55412));
#10695=EDGE_LOOP('',(#55413,#55414,#55415,#55416,#55417,#55418));
#16632=LINE('',#109664,#22666);
#16633=LINE('',#109688,#22667);
#16634=LINE('',#109736,#22668);
#16635=LINE('',#109784,#22669);
#16636=LINE('',#109838,#22670);
#16637=LINE('',#109886,#22671);
#16638=LINE('',#109934,#22672);
#16639=LINE('',#109988,#22673);
#16640=LINE('',#110035,#22674);
#16641=LINE('',#110055,#22675);
#16642=LINE('',#110080,#22676);
#16643=LINE('',#110105,#22677);
#16644=LINE('',#110129,#22678);
#16645=LINE('',#110154,#22679);
#16646=LINE('',#110179,#22680);
#16647=LINE('',#110941,#22681);
#16648=LINE('',#110943,#22682);
#16649=LINE('',#110945,#22683);
#16650=LINE('',#110946,#22684);
#16651=LINE('',#110949,#22685);
#16652=LINE('',#110951,#22686);
#16653=LINE('',#110952,#22687);
#16654=LINE('',#110955,#22688);
#16655=LINE('',#110957,#22689);
#16656=LINE('',#110958,#22690);
#16657=LINE('',#110961,#22691);
#16658=LINE('',#110963,#22692);
#16659=LINE('',#110964,#22693);
#16660=LINE('',#110967,#22694);
#16661=LINE('',#110969,#22695);
#16662=LINE('',#110970,#22696);
#16663=LINE('',#110972,#22697);
#16664=LINE('',#110973,#22698);
#16665=LINE('',#110979,#22699);
#16666=LINE('',#110985,#22700);
#22666=VECTOR('',#75160,0.999999999999996);
#22667=VECTOR('',#75165,0.999999999999996);
#22668=VECTOR('',#75168,0.999999999999996);
#22669=VECTOR('',#75171,0.999999999999996);
#22670=VECTOR('',#75174,0.999999999999996);
#22671=VECTOR('',#75177,0.999999999999996);
#22672=VECTOR('',#75180,0.999999999999996);
#22673=VECTOR('',#75183,0.999999999999996);
#22674=VECTOR('',#75188,0.739000000000001);
#22675=VECTOR('',#75193,0.739000000000001);
#22676=VECTOR('',#75196,0.739000000000001);
#22677=VECTOR('',#75199,0.739000000000001);
#22678=VECTOR('',#75202,0.739000000000001);
#22679=VECTOR('',#75205,0.739000000000001);
#22680=VECTOR('',#75208,0.739000000000001);
#22681=VECTOR('',#75225,10.);
#22682=VECTOR('',#75226,10.);
#22683=VECTOR('',#75227,10.);
#22684=VECTOR('',#75228,10.);
#22685=VECTOR('',#75231,10.);
#22686=VECTOR('',#75232,10.);
#22687=VECTOR('',#75233,10.);
#22688=VECTOR('',#75236,10.);
#22689=VECTOR('',#75237,10.);
#22690=VECTOR('',#75238,10.);
#22691=VECTOR('',#75241,10.);
#22692=VECTOR('',#75242,10.);
#22693=VECTOR('',#75243,10.);
#22694=VECTOR('',#75246,10.);
#22695=VECTOR('',#75247,10.);
#22696=VECTOR('',#75248,10.);
#22697=VECTOR('',#75251,10.);
#22698=VECTOR('',#75252,10.);
#22699=VECTOR('',#75261,0.899999999999999);
#22700=VECTOR('',#75270,1.45);
#24528=B_SPLINE_CURVE_WITH_KNOTS('',3,(#109666,#109667,#109668,#109669,
#109670,#109671,#109672,#109673,#109674,#109675),.UNSPECIFIED.,.F.,.F.,
(4,3,3,4),(-4.09157007060749,-3.96821312525615,-2.97615984394211,-2.0654640260217),
 .UNSPECIFIED.);
#24529=B_SPLINE_CURVE_WITH_KNOTS('',3,(#109678,#109679,#109680,#109681,
#109682,#109683,#109684),.UNSPECIFIED.,.F.,.F.,(4,3,4),(0.,0.992053281314042,
1.11548660900393),.UNSPECIFIED.);
#24530=B_SPLINE_CURVE_WITH_KNOTS('',3,(#109689,#109690,#109691,#109692,
#109693,#109694,#109695,#109696,#109697,#109698,#109699,#109700,#109701,
#109702,#109703,#109704,#109705,#109706,#109707,#109708,#109709,#109710),
 .UNSPECIFIED.,.F.,.F.,(4,3,3,3,3,3,3,4),(-10.3747553777871,-9.92053281314039,
-8.92847953182635,-7.93642625051231,-6.94437296919827,-5.95231968788423,
-4.96026640657019,-4.09157007060749),.UNSPECIFIED.);
#24531=B_SPLINE_CURVE_WITH_KNOTS('',3,(#109711,#109712,#109713,#109714,
#109715,#109716,#109717,#109718,#109719,#109720,#109721,#109722,#109723,
#109724,#109725,#109726,#109727,#109728,#109729,#109730,#109731,#109732),
 .UNSPECIFIED.,.F.,.F.,(4,3,3,3,3,3,3,4),(1.11548660900393,1.98410656262808,
2.97615984394212,3.96821312525616,4.9602664065702,5.95231968788424,6.94437296919828,
7.39867191618352),.UNSPECIFIED.);
#24532=B_SPLINE_CURVE_WITH_KNOTS('',3,(#109737,#109738,#109739,#109740,
#109741,#109742,#109743,#109744,#109745,#109746,#109747,#109748,#109749,
#109750,#109751,#109752,#109753,#109754,#109755,#109756,#109757,#109758),
 .UNSPECIFIED.,.F.,.F.,(4,3,3,3,3,3,3,4),(-16.6579406849665,-15.8728525010246,
-14.8807992197106,-13.8887459383965,-12.8966926570825,-11.9046393757685,
-10.9125860944544,-10.3747553777871),.UNSPECIFIED.);
#24533=B_SPLINE_CURVE_WITH_KNOTS('',3,(#109759,#109760,#109761,#109762,
#109763,#109764,#109765,#109766,#109767,#109768,#109769,#109770,#109771,
#109772,#109773,#109774,#109775,#109776,#109777,#109778,#109779,#109780),
 .UNSPECIFIED.,.F.,.F.,(4,3,3,3,3,3,3,4),(7.39867191618352,7.93642625051232,
8.92847953182636,9.9205328131404,10.9125860944544,11.9046393757685,12.8966926570825,
13.6818572233631),.UNSPECIFIED.);
#24534=B_SPLINE_CURVE_WITH_KNOTS('',3,(#109785,#109786,#109787,#109788,
#109789,#109790,#109791,#109792,#109793,#109794,#109795,#109796,#109797,
#109798,#109799,#109800,#109801,#109802,#109803,#109804,#109805,#109806,
#109807,#109808,#109809),.UNSPECIFIED.,.F.,.F.,(4,3,3,3,3,3,3,3,4),(-22.9411259921461,
-22.8172254702229,-21.8251721889089,-20.8331189075948,-19.8410656262808,
-18.8490123449667,-17.8569590636527,-16.8649057823387,-16.6579406849665),
 .UNSPECIFIED.);
#24535=B_SPLINE_CURVE_WITH_KNOTS('',3,(#109810,#109811,#109812,#109813,
#109814,#109815,#109816,#109817,#109818,#109819,#109820,#109821,#109822,
#109823,#109824,#109825,#109826,#109827,#109828,#109829,#109830,#109831,
#109832,#109833,#109834),.UNSPECIFIED.,.F.,.F.,(4,3,3,3,3,3,3,3,4),(13.6818572233631,
13.8887459383966,14.8807992197106,15.8728525010246,16.8649057823387,17.8569590636527,
18.8490123449668,19.8410656262808,19.9650425305427),.UNSPECIFIED.);
#24536=B_SPLINE_CURVE_WITH_KNOTS('',3,(#109839,#109840,#109841,#109842,
#109843,#109844,#109845,#109846,#109847,#109848,#109849,#109850,#109851,
#109852,#109853,#109854,#109855,#109856,#109857,#109858,#109859,#109860),
 .UNSPECIFIED.,.F.,.F.,(4,3,3,3,3,3,3,4),(-29.2243112993257,-28.7695451581071,
-27.7774918767931,-26.7854385954791,-25.793385314165,-24.801332032851,-23.8092787515369,
-22.9411259921461),.UNSPECIFIED.);
#24537=B_SPLINE_CURVE_WITH_KNOTS('',3,(#109861,#109862,#109863,#109864,
#109865,#109866,#109867,#109868,#109869,#109870,#109871,#109872,#109873,
#109874,#109875,#109876,#109877,#109878,#109879,#109880,#109881,#109882),
 .UNSPECIFIED.,.F.,.F.,(4,3,3,3,3,3,3,4),(19.9650425305427,20.8331189075948,
21.8251721889089,22.8172254702229,23.8092787515369,24.801332032851,25.793385314165,
26.2482278377223),.UNSPECIFIED.);
#24538=B_SPLINE_CURVE_WITH_KNOTS('',3,(#109887,#109888,#109889,#109890,
#109891,#109892,#109893,#109894,#109895,#109896,#109897,#109898,#109899,
#109900,#109901,#109902,#109903,#109904,#109905,#109906,#109907,#109908),
 .UNSPECIFIED.,.F.,.F.,(4,3,3,3,3,3,3,4),(-35.5074966065053,-34.7218648459914,
-33.7298115646773,-32.7377582833633,-31.7457050020492,-30.7536517207352,
-29.7615984394212,-29.2243112993257),.UNSPECIFIED.);
#24539=B_SPLINE_CURVE_WITH_KNOTS('',3,(#109909,#109910,#109911,#109912,
#109913,#109914,#109915,#109916,#109917,#109918,#109919,#109920,#109921,
#109922,#109923,#109924,#109925,#109926,#109927,#109928,#109929,#109930),
 .UNSPECIFIED.,.F.,.F.,(4,3,3,3,3,3,3,4),(26.2482278377223,26.7854385954791,
27.7774918767931,28.7695451581071,29.7615984394212,30.7536517207352,31.7457050020493,
32.5314131449019),.UNSPECIFIED.);
#24540=B_SPLINE_CURVE_WITH_KNOTS('',3,(#109935,#109936,#109937,#109938,
#109939,#109940,#109941,#109942,#109943,#109944,#109945,#109946,#109947,
#109948,#109949,#109950,#109951,#109952,#109953,#109954,#109955,#109956,
#109957,#109958,#109959),.UNSPECIFIED.,.F.,.F.,(4,3,3,3,3,3,3,3,4),(-41.7906819136849,
-41.6662378151896,-40.6741845338756,-39.6821312525616,-38.6900779712475,
-37.6980246899335,-36.7059714086194,-35.7139181273054,-35.5074966065053),
 .UNSPECIFIED.);
#24541=B_SPLINE_CURVE_WITH_KNOTS('',3,(#109960,#109961,#109962,#109963,
#109964,#109965,#109966,#109967,#109968,#109969,#109970,#109971,#109972,
#109973,#109974,#109975,#109976,#109977,#109978,#109979,#109980,#109981,
#109982,#109983,#109984),.UNSPECIFIED.,.F.,.F.,(4,3,3,3,3,3,3,3,4),(32.5314131449019,
32.7377582833633,33.7298115646773,34.7218648459914,35.7139181273054,36.7059714086195,
37.6980246899335,38.6900779712475,38.8145984520815),.UNSPECIFIED.);
#24542=B_SPLINE_CURVE_WITH_KNOTS('',3,(#109991,#109992,#109993,#109994,
#109995,#109996,#109997,#109998,#109999,#110000,#110001,#110002,#110003,
#110004,#110005,#110006,#110007,#110008,#110009),.UNSPECIFIED.,.F.,.F.,
(4,3,3,3,3,3,4),(-47.6185575030738,-46.6265042217598,-45.6344509404458,
-44.6423976591318,-43.6503443778177,-42.6582910965037,-41.7906819136849),
 .UNSPECIFIED.);
#24543=B_SPLINE_CURVE_WITH_KNOTS('',3,(#110010,#110011,#110012,#110013,
#110014,#110015,#110016,#110017,#110018,#110019,#110020,#110021,#110022,
#110023,#110024,#110025,#110026,#110027,#110028,#110029,#110030,#110031),
 .UNSPECIFIED.,.F.,.F.,(4,3,3,3,3,3,3,4),(38.8145984520815,39.6821312525616,
40.6741845338756,41.6662378151897,42.6582910965037,43.6503443778177,44.6423976591318,
45.0977837592611),.UNSPECIFIED.);
#24544=B_SPLINE_CURVE_WITH_KNOTS('',3,(#110037,#110038,#110039,#110040,
#110041,#110042,#110043),.UNSPECIFIED.,.F.,.F.,(4,1,1,1,4),(53.4070751110264,
54.2746842938452,55.2667375751592,56.2587908564733,57.1694866743937),
 .UNSPECIFIED.);
#24545=B_SPLINE_CURVE_WITH_KNOTS('',3,(#110046,#110047,#110048,#110049,
#110050,#110051),.UNSPECIFIED.,.F.,.F.,(4,1,1,4),(53.4070751110264,53.9437422922112,
54.9357955735252,55.9278488548392),.UNSPECIFIED.);
#24546=B_SPLINE_CURVE_WITH_KNOTS('',3,(#110056,#110057,#110058,#110059,
#110060,#110061,#110062,#110063,#110064,#110065,#110066),.UNSPECIFIED.,
 .F.,.F.,(4,1,1,1,1,1,1,1,4),(47.1238898038469,47.3303113246469,48.322364605961,
49.314417887275,50.306471168589,51.2985244499031,52.2905777312171,53.2826310125312,
53.4070751110264),.UNSPECIFIED.);
#24547=B_SPLINE_CURVE_WITH_KNOTS('',3,(#110067,#110068,#110069,#110070,
#110071,#110072,#110073,#110074,#110075,#110076),.UNSPECIFIED.,.F.,.F.,
(4,1,1,1,1,1,1,4),(47.1238898038469,47.9914226043269,48.983475885641,49.975529166955,
50.967582448269,51.9596357295831,52.9516890108971,53.4070751110264),
 .UNSPECIFIED.);
#24548=B_SPLINE_CURVE_WITH_KNOTS('',3,(#110081,#110082,#110083,#110084,
#110085,#110086,#110087,#110088,#110089,#110090),.UNSPECIFIED.,.F.,.F.,
(4,1,1,1,1,1,1,4),(40.8407044966673,41.3779916367627,42.3700449180767,43.3620981993908,
44.3541514807048,45.3462047620188,46.3382580433329,47.1238898038469),
 .UNSPECIFIED.);
#24549=B_SPLINE_CURVE_WITH_KNOTS('',3,(#110091,#110092,#110093,#110094,
#110095,#110096,#110097,#110098,#110099,#110100,#110101),.UNSPECIFIED.,
 .F.,.F.,(4,1,1,1,1,1,1,1,4),(40.8407044966673,41.0470496351287,42.0391029164427,
43.0311561977567,44.0232094790708,45.0152627603848,46.0073160416989,46.9993693230129,
47.1238898038469),.UNSPECIFIED.);
#24550=B_SPLINE_CURVE_WITH_KNOTS('',3,(#110106,#110107,#110108,#110109,
#110110,#110111,#110112,#110113,#110114,#110115),.UNSPECIFIED.,.F.,.F.,
(4,1,1,1,1,1,1,4),(34.5575191894877,35.4256719488784,36.4177252301925,37.4097785115065,
38.4018317928206,39.3938850741346,40.3859383554486,40.8407044966673),
 .UNSPECIFIED.);
#24551=B_SPLINE_CURVE_WITH_KNOTS('',3,(#110116,#110117,#110118,#110119,
#110120,#110121,#110122,#110123,#110124,#110125),.UNSPECIFIED.,.F.,.F.,
(4,1,1,1,1,1,1,4),(34.5575191894877,35.0947299472444,36.0867832285585,37.0788365098725,
38.0708897911865,39.0629430725006,40.0549963538146,40.8407044966673),
 .UNSPECIFIED.);
#24552=B_SPLINE_CURVE_WITH_KNOTS('',3,(#110130,#110131,#110132,#110133,
#110134,#110135,#110136,#110137,#110138,#110139,#110140),.UNSPECIFIED.,
 .F.,.F.,(4,1,1,1,1,1,1,1,4),(28.2743338823081,28.4812989796802,29.4733522609942,
30.4654055423083,31.4574588236223,32.4495121049363,33.4415653862504,34.4336186675644,
34.5575191894877),.UNSPECIFIED.);
#24553=B_SPLINE_CURVE_WITH_KNOTS('',3,(#110141,#110142,#110143,#110144,
#110145,#110146,#110147,#110148,#110149,#110150),.UNSPECIFIED.,.F.,.F.,
(4,1,1,1,1,1,1,4),(28.2743338823081,29.1424102593602,30.1344635406742,31.1265168219883,
32.1185701033023,33.1106233846163,34.1026766659304,34.5575191894877),
 .UNSPECIFIED.);
#24554=B_SPLINE_CURVE_WITH_KNOTS('',3,(#110155,#110156,#110157,#110158,
#110159,#110160,#110161,#110162,#110163,#110164),.UNSPECIFIED.,.F.,.F.,
(4,1,1,1,1,1,1,4),(21.9911485751285,22.5289792917959,23.52103257311,24.513085854424,
25.5051391357381,26.4971924170521,27.4892456983661,28.2743338823081),
 .UNSPECIFIED.);
#24555=B_SPLINE_CURVE_WITH_KNOTS('',3,(#110165,#110166,#110167,#110168,
#110169,#110170,#110171,#110172,#110173,#110174,#110175),.UNSPECIFIED.,
 .F.,.F.,(4,1,1,1,1,1,1,1,4),(21.9911485751285,22.1980372901619,23.1900905714759,
24.18214385279,25.174197134104,26.1662504154181,27.1583036967321,28.1503569780461,
28.2743338823081),.UNSPECIFIED.);
#24556=B_SPLINE_CURVE_WITH_KNOTS('',3,(#110180,#110181,#110182,#110183,
#110184,#110185,#110186,#110187,#110188,#110189),.UNSPECIFIED.,.F.,.F.,
(4,1,1,1,1,1,1,4),(15.7079632679489,16.5766596039117,17.5687128852257,18.5607661665398,
19.5528194478538,20.5448727291679,21.5369260104819,21.9911485751285),
 .UNSPECIFIED.);
#24557=B_SPLINE_CURVE_WITH_KNOTS('',3,(#110190,#110191,#110192,#110193,
#110194,#110195,#110196,#110197,#110198,#110199),.UNSPECIFIED.,.F.,.F.,
(4,1,1,1,1,1,1,4),(15.7079632679489,16.2457176022777,17.2377708835917,18.2298241649058,
19.2218774462198,20.2139307275338,21.2059840088479,21.9911485751285),
 .UNSPECIFIED.);
#24558=B_SPLINE_CURVE_WITH_KNOTS('',3,(#110201,#110202,#110203,#110204,
#110205,#110206,#110207,#110208,#110209,#110210,#110211,#110212,#110213,
#110214,#110215,#110216,#110217,#110218,#110219,#110220,#110221,#110222,
#110223,#110224,#110225,#110226,#110227,#110228,#110229,#110230,#110231,
#110232,#110233,#110234,#110235,#110236,#110237,#110238,#110239,#110240,
#110241,#110242,#110243,#110244,#110245,#110246,#110247,#110248,#110249,
#110250,#110251,#110252,#110253,#110254,#110255,#110256,#110257,#110258,
#110259,#110260,#110261,#110262,#110263,#110264,#110265,#110266,#110267,
#110268,#110269,#110270,#110271,#110272,#110273),.UNSPECIFIED.,.F.,.F.,
(4,3,3,3,3,3,3,3,3,3,3,3,3,3,3,3,3,3,3,3,3,3,3,3,4),(-0.178587760439504,
-0.172436005266845,-0.162325405279674,-0.158983610121922,-0.156300142716475,
-0.145521462210125,-0.137695659081724,-0.13518810584043,-0.123840773922177,
-0.112407563090991,-0.106415995852445,-0.103612144676863,-0.0915512053694793,
-0.0801073046982944,-0.0748685857871388,-0.0720605549642836,-0.0695158393189569,
-0.057554069888016,-0.0453143736546683,-0.0394431135780157,-0.0369681942630705,
-0.0343654591089171,-0.0216730559581644,-0.0090670142413088,0.),
 .UNSPECIFIED.);
#24559=B_SPLINE_CURVE_WITH_KNOTS('',3,(#110276,#110277,#110278,#110279,
#110280,#110281,#110282,#110283,#110284,#110285,#110286,#110287,#110288,
#110289,#110290,#110291,#110292,#110293,#110294,#110295,#110296,#110297,
#110298,#110299,#110300,#110301,#110302,#110303,#110304,#110305,#110306,
#110307,#110308,#110309,#110310,#110311,#110312,#110313,#110314,#110315,
#110316,#110317,#110318,#110319,#110320,#110321,#110322,#110323,#110324,
#110325,#110326,#110327,#110328,#110329,#110330,#110331,#110332,#110333,
#110334,#110335,#110336,#110337,#110338,#110339,#110340,#110341,#110342,
#110343,#110344,#110345,#110346,#110347,#110348,#110349,#110350,#110351),
 .UNSPECIFIED.,.F.,.F.,(4,3,3,3,3,3,3,3,3,3,3,3,3,3,3,3,3,3,3,3,3,3,3,3,
3,4),(-0.177567088092197,-0.169718205449901,-0.158456796357131,-0.154087938332518,
-0.149901326685707,-0.137441206344475,-0.130214422139883,-0.127484197404693,
-0.124915045826681,-0.112965831709766,-0.101293012250859,-0.0956918677235842,
-0.0932236527120616,-0.0908269354509327,-0.0796269327077398,-0.0694129961400613,
-0.0639913339275198,-0.0605457458673101,-0.0580972397750422,-0.0469085861859489,
-0.0358589547005544,-0.0306372080887885,-0.0277838560902035,-0.017202291045908,
-0.00700607863093054,0.),.UNSPECIFIED.);
#24560=B_SPLINE_CURVE_WITH_KNOTS('',3,(#110556,#110557,#110558,#110559),
 .UNSPECIFIED.,.F.,.F.,(4,4),(45.0977837592611,45.553093477052),
 .UNSPECIFIED.);
#24561=B_SPLINE_CURVE_WITH_KNOTS('',3,(#110561,#110562,#110563,#110564,
#110565,#110566,#110567,#110568,#110569,#110570,#110571,#110572,#110573,
#110574,#110575,#110576,#110577,#110578,#110579,#110580,#110581,#110582,
#110583,#110584,#110585,#110586,#110587,#110588,#110589,#110590,#110591,
#110592,#110593,#110594,#110595,#110596,#110597,#110598,#110599,#110600,
#110601,#110602,#110603,#110604,#110605,#110606,#110607,#110608,#110609,
#110610,#110611,#110612,#110613,#110614,#110615,#110616,#110617,#110618,
#110619,#110620,#110621,#110622,#110623,#110624,#110625,#110626,#110627,
#110628,#110629,#110630,#110631,#110632,#110633),.UNSPECIFIED.,.F.,.F.,
(4,3,3,3,3,3,3,3,3,3,3,3,3,3,3,3,3,3,3,3,3,3,3,3,4),(-0.17858776043956,
-0.172436005266898,-0.162325405279723,-0.158983610459464,-0.156300143130782,
-0.14552146303087,-0.137695660713911,-0.135188108280273,-0.123840776492776,
-0.112407565558593,-0.10641599916013,-0.103612145963209,-0.091551205369502,
-0.0801073046983142,-0.0748685855925244,-0.0720605538167012,-0.0695158390600375,
-0.0575540698726435,-0.0453143738867585,-0.0394431138098223,-0.0369681938209412,
-0.0343654589710512,-0.0216730560122649,-0.00906701360523848,0.),
 .UNSPECIFIED.);
#24562=B_SPLINE_CURVE_WITH_KNOTS('',3,(#110634,#110635,#110636,#110637,
#110638,#110639,#110640,#110641,#110642),.UNSPECIFIED.,.F.,.F.,(4,1,1,1,
1,1,4),(10.3747553777871,11.2854511957075,12.2775044770215,13.2695577583356,
14.2616110396496,15.2536643209636,15.7079632679489),.UNSPECIFIED.);
#24563=B_SPLINE_CURVE_WITH_KNOTS('',3,(#110648,#110649,#110650,#110651,
#110652,#110653,#110654,#110655,#110656,#110657,#110658,#110659,#110660,
#110661,#110662,#110663,#110664,#110665,#110666,#110667,#110668,#110669,
#110670,#110671,#110672,#110673,#110674,#110675,#110676,#110677,#110678,
#110679,#110680,#110681,#110682,#110683,#110684,#110685,#110686,#110687,
#110688,#110689,#110690,#110691,#110692,#110693,#110694,#110695,#110696,
#110697,#110698,#110699,#110700,#110701,#110702,#110703,#110704,#110705,
#110706,#110707,#110708,#110709,#110710,#110711,#110712,#110713,#110714,
#110715,#110716,#110717,#110718,#110719,#110720,#110721,#110722,#110723),
 .UNSPECIFIED.,.F.,.F.,(4,3,3,3,3,3,3,3,3,3,3,3,3,3,3,3,3,3,3,3,3,3,3,3,
3,4),(-0.177567088092152,-0.169718205449872,-0.158456796357106,-0.154087938106763,
-0.149901326639656,-0.137441206226106,-0.130214422036311,-0.127484196657443,
-0.124915044564136,-0.112965830066187,-0.101293009880069,-0.0956918649462959,
-0.0932236438564468,-0.0908269205250241,-0.0796269327077417,-0.0694130001063571,
-0.0639913397708145,-0.0605456801771174,-0.0580972309446734,-0.046908577415714,
-0.0358589469260566,-0.0306371966909039,-0.0277838544508456,-0.01720229026982,
-0.00700607908527243,0.),.UNSPECIFIED.);
#24564=B_SPLINE_CURVE_WITH_KNOTS('',3,(#110726,#110727,#110728,#110729,
#110730,#110731,#110732,#110733),.UNSPECIFIED.,.F.,.F.,(4,1,1,1,1,4),(11.6163931973415,
12.6084464786556,13.6004997599696,14.5925530412836,15.5846063225977,15.7079632679489),
 .UNSPECIFIED.);
#29974=VERTEX_POINT('',#109662);
#29975=VERTEX_POINT('',#109663);
#29976=VERTEX_POINT('',#109665);
#29977=VERTEX_POINT('',#109676);
#29978=VERTEX_POINT('',#109686);
#29979=VERTEX_POINT('',#109687);
#29980=VERTEX_POINT('',#109734);
#29981=VERTEX_POINT('',#109735);
#29982=VERTEX_POINT('',#109782);
#29983=VERTEX_POINT('',#109783);
#29984=VERTEX_POINT('',#109836);
#29985=VERTEX_POINT('',#109837);
#29986=VERTEX_POINT('',#109884);
#29987=VERTEX_POINT('',#109885);
#29988=VERTEX_POINT('',#109932);
#29989=VERTEX_POINT('',#109933);
#29990=VERTEX_POINT('',#109986);
#29991=VERTEX_POINT('',#109987);
#29992=VERTEX_POINT('',#109989);
#29993=VERTEX_POINT('',#110033);
#29994=VERTEX_POINT('',#110034);
#29995=VERTEX_POINT('',#110036);
#29996=VERTEX_POINT('',#110044);
#29997=VERTEX_POINT('',#110053);
#29998=VERTEX_POINT('',#110054);
#29999=VERTEX_POINT('',#110078);
#30000=VERTEX_POINT('',#110079);
#30001=VERTEX_POINT('',#110103);
#30002=VERTEX_POINT('',#110104);
#30003=VERTEX_POINT('',#110127);
#30004=VERTEX_POINT('',#110128);
#30005=VERTEX_POINT('',#110152);
#30006=VERTEX_POINT('',#110153);
#30007=VERTEX_POINT('',#110177);
#30008=VERTEX_POINT('',#110178);
#30009=VERTEX_POINT('',#110274);
#30010=VERTEX_POINT('',#110560);
#30011=VERTEX_POINT('',#110644);
#30012=VERTEX_POINT('',#110647);
#30013=VERTEX_POINT('',#110939);
#30014=VERTEX_POINT('',#110940);
#30015=VERTEX_POINT('',#110942);
#30016=VERTEX_POINT('',#110944);
#30017=VERTEX_POINT('',#110948);
#30018=VERTEX_POINT('',#110950);
#30019=VERTEX_POINT('',#110954);
#30020=VERTEX_POINT('',#110956);
#30021=VERTEX_POINT('',#110960);
#30022=VERTEX_POINT('',#110962);
#30023=VERTEX_POINT('',#110966);
#30024=VERTEX_POINT('',#110968);
#30025=VERTEX_POINT('',#110976);
#30026=VERTEX_POINT('',#110983);
#38460=EDGE_CURVE('',#29974,#29975,#16632,.T.);
#38461=EDGE_CURVE('',#29974,#29976,#24528,.T.);
#38462=EDGE_CURVE('',#29976,#29977,#1420,.T.);
#38463=EDGE_CURVE('',#29977,#29975,#24529,.T.);
#38464=EDGE_CURVE('',#29978,#29979,#16633,.T.);
#38465=EDGE_CURVE('',#29978,#29974,#24530,.T.);
#38466=EDGE_CURVE('',#29975,#29979,#24531,.T.);
#38467=EDGE_CURVE('',#29980,#29981,#16634,.T.);
#38468=EDGE_CURVE('',#29980,#29978,#24532,.T.);
#38469=EDGE_CURVE('',#29979,#29981,#24533,.T.);
#38470=EDGE_CURVE('',#29982,#29983,#16635,.T.);
#38471=EDGE_CURVE('',#29982,#29980,#24534,.T.);
#38472=EDGE_CURVE('',#29981,#29983,#24535,.T.);
#38473=EDGE_CURVE('',#29984,#29985,#16636,.T.);
#38474=EDGE_CURVE('',#29984,#29982,#24536,.T.);
#38475=EDGE_CURVE('',#29983,#29985,#24537,.T.);
#38476=EDGE_CURVE('',#29986,#29987,#16637,.T.);
#38477=EDGE_CURVE('',#29986,#29984,#24538,.T.);
#38478=EDGE_CURVE('',#29985,#29987,#24539,.T.);
#38479=EDGE_CURVE('',#29988,#29989,#16638,.T.);
#38480=EDGE_CURVE('',#29988,#29986,#24540,.T.);
#38481=EDGE_CURVE('',#29987,#29989,#24541,.T.);
#38482=EDGE_CURVE('',#29990,#29991,#16639,.T.);
#38483=EDGE_CURVE('',#29992,#29990,#1421,.T.);
#38484=EDGE_CURVE('',#29992,#29988,#24542,.T.);
#38485=EDGE_CURVE('',#29989,#29991,#24543,.T.);
#38486=EDGE_CURVE('',#29993,#29994,#16640,.T.);
#38487=EDGE_CURVE('',#29993,#29995,#24544,.T.);
#38488=EDGE_CURVE('',#29996,#29995,#1422,.T.);
#38489=EDGE_CURVE('',#29994,#29996,#24545,.T.);
#38490=EDGE_CURVE('',#29997,#29998,#16641,.T.);
#38491=EDGE_CURVE('',#29997,#29993,#24546,.T.);
#38492=EDGE_CURVE('',#29998,#29994,#24547,.T.);
#38493=EDGE_CURVE('',#29999,#30000,#16642,.T.);
#38494=EDGE_CURVE('',#29999,#29997,#24548,.T.);
#38495=EDGE_CURVE('',#30000,#29998,#24549,.T.);
#38496=EDGE_CURVE('',#30001,#30002,#16643,.T.);
#38497=EDGE_CURVE('',#30001,#29999,#24550,.T.);
#38498=EDGE_CURVE('',#30002,#30000,#24551,.T.);
#38499=EDGE_CURVE('',#30003,#30004,#16644,.T.);
#38500=EDGE_CURVE('',#30003,#30001,#24552,.T.);
#38501=EDGE_CURVE('',#30004,#30002,#24553,.T.);
#38502=EDGE_CURVE('',#30005,#30006,#16645,.T.);
#38503=EDGE_CURVE('',#30005,#30003,#24554,.T.);
#38504=EDGE_CURVE('',#30006,#30004,#24555,.T.);
#38505=EDGE_CURVE('',#30007,#30008,#16646,.T.);
#38506=EDGE_CURVE('',#30007,#30005,#24556,.T.);
#38507=EDGE_CURVE('',#30008,#30006,#24557,.T.);
#38508=EDGE_CURVE('',#29995,#29992,#24558,.T.);
#38509=EDGE_CURVE('',#30009,#29992,#1423,.T.);
#38510=EDGE_CURVE('',#30009,#29996,#24559,.T.);
#38511=EDGE_CURVE('',#29991,#30009,#24560,.T.);
#38512=EDGE_CURVE('',#30010,#29977,#24561,.T.);
#38513=EDGE_CURVE('',#30010,#30008,#24562,.T.);
#38514=EDGE_CURVE('',#29977,#30011,#1424,.T.);
#38515=EDGE_CURVE('',#30011,#29976,#1425,.T.);
#38516=EDGE_CURVE('',#29976,#30012,#24563,.T.);
#38517=EDGE_CURVE('',#30012,#30010,#1426,.T.);
#38518=EDGE_CURVE('',#30012,#30007,#24564,.T.);
#38519=EDGE_CURVE('',#30013,#30014,#16647,.T.);
#38520=EDGE_CURVE('',#30013,#30015,#16648,.T.);
#38521=EDGE_CURVE('',#30015,#30016,#16649,.T.);
#38522=EDGE_CURVE('',#30014,#30016,#16650,.T.);
#38523=EDGE_CURVE('',#30017,#30013,#16651,.T.);
#38524=EDGE_CURVE('',#30017,#30018,#16652,.T.);
#38525=EDGE_CURVE('',#30018,#30015,#16653,.T.);
#38526=EDGE_CURVE('',#30019,#30017,#16654,.T.);
#38527=EDGE_CURVE('',#30019,#30020,#16655,.T.);
#38528=EDGE_CURVE('',#30020,#30018,#16656,.T.);
#38529=EDGE_CURVE('',#30021,#30019,#16657,.T.);
#38530=EDGE_CURVE('',#30021,#30022,#16658,.T.);
#38531=EDGE_CURVE('',#30022,#30020,#16659,.T.);
#38532=EDGE_CURVE('',#30023,#30021,#16660,.T.);
#38533=EDGE_CURVE('',#30023,#30024,#16661,.T.);
#38534=EDGE_CURVE('',#30024,#30022,#16662,.T.);
#38535=EDGE_CURVE('',#30014,#30023,#16663,.T.);
#38536=EDGE_CURVE('',#30016,#30024,#16664,.T.);
#38537=EDGE_CURVE('',#30025,#30025,#1427,.T.);
#38538=EDGE_CURVE('',#30011,#30025,#16665,.T.);
#38539=EDGE_CURVE('',#29990,#30009,#1428,.T.);
#38540=EDGE_CURVE('',#30026,#30026,#1429,.T.);
#38541=EDGE_CURVE('',#30026,#29990,#16666,.T.);
#55255=ORIENTED_EDGE('',*,*,#38460,.F.);
#55256=ORIENTED_EDGE('',*,*,#38461,.T.);
#55257=ORIENTED_EDGE('',*,*,#38462,.T.);
#55258=ORIENTED_EDGE('',*,*,#38463,.T.);
#55259=ORIENTED_EDGE('',*,*,#38464,.F.);
#55260=ORIENTED_EDGE('',*,*,#38465,.T.);
#55261=ORIENTED_EDGE('',*,*,#38460,.T.);
#55262=ORIENTED_EDGE('',*,*,#38466,.T.);
#55263=ORIENTED_EDGE('',*,*,#38467,.F.);
#55264=ORIENTED_EDGE('',*,*,#38468,.T.);
#55265=ORIENTED_EDGE('',*,*,#38464,.T.);
#55266=ORIENTED_EDGE('',*,*,#38469,.T.);
#55267=ORIENTED_EDGE('',*,*,#38470,.F.);
#55268=ORIENTED_EDGE('',*,*,#38471,.T.);
#55269=ORIENTED_EDGE('',*,*,#38467,.T.);
#55270=ORIENTED_EDGE('',*,*,#38472,.T.);
#55271=ORIENTED_EDGE('',*,*,#38473,.F.);
#55272=ORIENTED_EDGE('',*,*,#38474,.T.);
#55273=ORIENTED_EDGE('',*,*,#38470,.T.);
#55274=ORIENTED_EDGE('',*,*,#38475,.T.);
#55275=ORIENTED_EDGE('',*,*,#38476,.F.);
#55276=ORIENTED_EDGE('',*,*,#38477,.T.);
#55277=ORIENTED_EDGE('',*,*,#38473,.T.);
#55278=ORIENTED_EDGE('',*,*,#38478,.T.);
#55279=ORIENTED_EDGE('',*,*,#38479,.F.);
#55280=ORIENTED_EDGE('',*,*,#38480,.T.);
#55281=ORIENTED_EDGE('',*,*,#38476,.T.);
#55282=ORIENTED_EDGE('',*,*,#38481,.T.);
#55283=ORIENTED_EDGE('',*,*,#38482,.F.);
#55284=ORIENTED_EDGE('',*,*,#38483,.F.);
#55285=ORIENTED_EDGE('',*,*,#38484,.T.);
#55286=ORIENTED_EDGE('',*,*,#38479,.T.);
#55287=ORIENTED_EDGE('',*,*,#38485,.T.);
#55288=ORIENTED_EDGE('',*,*,#38486,.F.);
#55289=ORIENTED_EDGE('',*,*,#38487,.T.);
#55290=ORIENTED_EDGE('',*,*,#38488,.F.);
#55291=ORIENTED_EDGE('',*,*,#38489,.F.);
#55292=ORIENTED_EDGE('',*,*,#38490,.F.);
#55293=ORIENTED_EDGE('',*,*,#38491,.T.);
#55294=ORIENTED_EDGE('',*,*,#38486,.T.);
#55295=ORIENTED_EDGE('',*,*,#38492,.F.);
#55296=ORIENTED_EDGE('',*,*,#38493,.F.);
#55297=ORIENTED_EDGE('',*,*,#38494,.T.);
#55298=ORIENTED_EDGE('',*,*,#38490,.T.);
#55299=ORIENTED_EDGE('',*,*,#38495,.F.);
#55300=ORIENTED_EDGE('',*,*,#38496,.F.);
#55301=ORIENTED_EDGE('',*,*,#38497,.T.);
#55302=ORIENTED_EDGE('',*,*,#38493,.T.);
#55303=ORIENTED_EDGE('',*,*,#38498,.F.);
#55304=ORIENTED_EDGE('',*,*,#38499,.F.);
#55305=ORIENTED_EDGE('',*,*,#38500,.T.);
#55306=ORIENTED_EDGE('',*,*,#38496,.T.);
#55307=ORIENTED_EDGE('',*,*,#38501,.F.);
#55308=ORIENTED_EDGE('',*,*,#38502,.F.);
#55309=ORIENTED_EDGE('',*,*,#38503,.T.);
#55310=ORIENTED_EDGE('',*,*,#38499,.T.);
#55311=ORIENTED_EDGE('',*,*,#38504,.F.);
#55312=ORIENTED_EDGE('',*,*,#38505,.F.);
#55313=ORIENTED_EDGE('',*,*,#38506,.T.);
#55314=ORIENTED_EDGE('',*,*,#38502,.T.);
#55315=ORIENTED_EDGE('',*,*,#38507,.F.);
#55316=ORIENTED_EDGE('',*,*,#38488,.T.);
#55317=ORIENTED_EDGE('',*,*,#38508,.T.);
#55318=ORIENTED_EDGE('',*,*,#38509,.F.);
#55319=ORIENTED_EDGE('',*,*,#38510,.T.);
#55320=ORIENTED_EDGE('',*,*,#38510,.F.);
#55321=ORIENTED_EDGE('',*,*,#38511,.F.);
#55322=ORIENTED_EDGE('',*,*,#38485,.F.);
#55323=ORIENTED_EDGE('',*,*,#38481,.F.);
#55324=ORIENTED_EDGE('',*,*,#38478,.F.);
#55325=ORIENTED_EDGE('',*,*,#38475,.F.);
#55326=ORIENTED_EDGE('',*,*,#38472,.F.);
#55327=ORIENTED_EDGE('',*,*,#38469,.F.);
#55328=ORIENTED_EDGE('',*,*,#38466,.F.);
#55329=ORIENTED_EDGE('',*,*,#38463,.F.);
#55330=ORIENTED_EDGE('',*,*,#38512,.F.);
#55331=ORIENTED_EDGE('',*,*,#38513,.T.);
#55332=ORIENTED_EDGE('',*,*,#38507,.T.);
#55333=ORIENTED_EDGE('',*,*,#38504,.T.);
#55334=ORIENTED_EDGE('',*,*,#38501,.T.);
#55335=ORIENTED_EDGE('',*,*,#38498,.T.);
#55336=ORIENTED_EDGE('',*,*,#38495,.T.);
#55337=ORIENTED_EDGE('',*,*,#38492,.T.);
#55338=ORIENTED_EDGE('',*,*,#38489,.T.);
#55339=ORIENTED_EDGE('',*,*,#38514,.T.);
#55340=ORIENTED_EDGE('',*,*,#38515,.T.);
#55341=ORIENTED_EDGE('',*,*,#38516,.T.);
#55342=ORIENTED_EDGE('',*,*,#38517,.T.);
#55343=ORIENTED_EDGE('',*,*,#38512,.T.);
#55344=ORIENTED_EDGE('',*,*,#38505,.T.);
#55345=ORIENTED_EDGE('',*,*,#38513,.F.);
#55346=ORIENTED_EDGE('',*,*,#38517,.F.);
#55347=ORIENTED_EDGE('',*,*,#38518,.T.);
#55348=ORIENTED_EDGE('',*,*,#38508,.F.);
#55349=ORIENTED_EDGE('',*,*,#38487,.F.);
#55350=ORIENTED_EDGE('',*,*,#38491,.F.);
#55351=ORIENTED_EDGE('',*,*,#38494,.F.);
#55352=ORIENTED_EDGE('',*,*,#38497,.F.);
#55353=ORIENTED_EDGE('',*,*,#38500,.F.);
#55354=ORIENTED_EDGE('',*,*,#38503,.F.);
#55355=ORIENTED_EDGE('',*,*,#38506,.F.);
#55356=ORIENTED_EDGE('',*,*,#38518,.F.);
#55357=ORIENTED_EDGE('',*,*,#38516,.F.);
#55358=ORIENTED_EDGE('',*,*,#38461,.F.);
#55359=ORIENTED_EDGE('',*,*,#38465,.F.);
#55360=ORIENTED_EDGE('',*,*,#38468,.F.);
#55361=ORIENTED_EDGE('',*,*,#38471,.F.);
#55362=ORIENTED_EDGE('',*,*,#38474,.F.);
#55363=ORIENTED_EDGE('',*,*,#38477,.F.);
#55364=ORIENTED_EDGE('',*,*,#38480,.F.);
#55365=ORIENTED_EDGE('',*,*,#38484,.F.);
#55366=ORIENTED_EDGE('',*,*,#38519,.F.);
#55367=ORIENTED_EDGE('',*,*,#38520,.T.);
#55368=ORIENTED_EDGE('',*,*,#38521,.T.);
#55369=ORIENTED_EDGE('',*,*,#38522,.F.);
#55370=ORIENTED_EDGE('',*,*,#38523,.F.);
#55371=ORIENTED_EDGE('',*,*,#38524,.T.);
#55372=ORIENTED_EDGE('',*,*,#38525,.T.);
#55373=ORIENTED_EDGE('',*,*,#38520,.F.);
#55374=ORIENTED_EDGE('',*,*,#38526,.F.);
#55375=ORIENTED_EDGE('',*,*,#38527,.T.);
#55376=ORIENTED_EDGE('',*,*,#38528,.T.);
#55377=ORIENTED_EDGE('',*,*,#38524,.F.);
#55378=ORIENTED_EDGE('',*,*,#38529,.F.);
#55379=ORIENTED_EDGE('',*,*,#38530,.T.);
#55380=ORIENTED_EDGE('',*,*,#38531,.T.);
#55381=ORIENTED_EDGE('',*,*,#38527,.F.);
#55382=ORIENTED_EDGE('',*,*,#38532,.F.);
#55383=ORIENTED_EDGE('',*,*,#38533,.T.);
#55384=ORIENTED_EDGE('',*,*,#38534,.T.);
#55385=ORIENTED_EDGE('',*,*,#38530,.F.);
#55386=ORIENTED_EDGE('',*,*,#38535,.F.);
#55387=ORIENTED_EDGE('',*,*,#38522,.T.);
#55388=ORIENTED_EDGE('',*,*,#38536,.T.);
#55389=ORIENTED_EDGE('',*,*,#38533,.F.);
#55390=ORIENTED_EDGE('',*,*,#38536,.F.);
#55391=ORIENTED_EDGE('',*,*,#38521,.F.);
#55392=ORIENTED_EDGE('',*,*,#38525,.F.);
#55393=ORIENTED_EDGE('',*,*,#38528,.F.);
#55394=ORIENTED_EDGE('',*,*,#38531,.F.);
#55395=ORIENTED_EDGE('',*,*,#38534,.F.);
#55396=ORIENTED_EDGE('',*,*,#38537,.F.);
#55397=ORIENTED_EDGE('',*,*,#38514,.F.);
#55398=ORIENTED_EDGE('',*,*,#38462,.F.);
#55399=ORIENTED_EDGE('',*,*,#38515,.F.);
#55400=ORIENTED_EDGE('',*,*,#38538,.T.);
#55401=ORIENTED_EDGE('',*,*,#38537,.T.);
#55402=ORIENTED_EDGE('',*,*,#38538,.F.);
#55403=ORIENTED_EDGE('',*,*,#38482,.T.);
#55404=ORIENTED_EDGE('',*,*,#38511,.T.);
#55405=ORIENTED_EDGE('',*,*,#38539,.F.);
#55406=ORIENTED_EDGE('',*,*,#38540,.F.);
#55407=ORIENTED_EDGE('',*,*,#38541,.T.);
#55408=ORIENTED_EDGE('',*,*,#38539,.T.);
#55409=ORIENTED_EDGE('',*,*,#38509,.T.);
#55410=ORIENTED_EDGE('',*,*,#38483,.T.);
#55411=ORIENTED_EDGE('',*,*,#38541,.F.);
#55412=ORIENTED_EDGE('',*,*,#38540,.T.);
#55413=ORIENTED_EDGE('',*,*,#38519,.T.);
#55414=ORIENTED_EDGE('',*,*,#38535,.T.);
#55415=ORIENTED_EDGE('',*,*,#38532,.T.);
#55416=ORIENTED_EDGE('',*,*,#38529,.T.);
#55417=ORIENTED_EDGE('',*,*,#38526,.T.);
#55418=ORIENTED_EDGE('',*,*,#38523,.T.);
#57121=B_SPLINE_SURFACE_WITH_KNOTS('',3,3,((#110352,#110353,#110354,#110355,
#110356,#110357,#110358,#110359,#110360,#110361,#110362,#110363,#110364,
#110365,#110366,#110367,#110368,#110369,#110370,#110371,#110372,#110373,
#110374,#110375,#110376,#110377,#110378,#110379,#110380,#110381,#110382,
#110383,#110384,#110385,#110386,#110387,#110388,#110389,#110390,#110391,
#110392,#110393,#110394,#110395,#110396,#110397,#110398,#110399,#110400,
#110401,#110402),(#110403,#110404,#110405,#110406,#110407,#110408,#110409,
#110410,#110411,#110412,#110413,#110414,#110415,#110416,#110417,#110418,
#110419,#110420,#110421,#110422,#110423,#110424,#110425,#110426,#110427,
#110428,#110429,#110430,#110431,#110432,#110433,#110434,#110435,#110436,
#110437,#110438,#110439,#110440,#110441,#110442,#110443,#110444,#110445,
#110446,#110447,#110448,#110449,#110450,#110451,#110452,#110453),(#110454,
#110455,#110456,#110457,#110458,#110459,#110460,#110461,#110462,#110463,
#110464,#110465,#110466,#110467,#110468,#110469,#110470,#110471,#110472,
#110473,#110474,#110475,#110476,#110477,#110478,#110479,#110480,#110481,
#110482,#110483,#110484,#110485,#110486,#110487,#110488,#110489,#110490,
#110491,#110492,#110493,#110494,#110495,#110496,#110497,#110498,#110499,
#110500,#110501,#110502,#110503,#110504),(#110505,#110506,#110507,#110508,
#110509,#110510,#110511,#110512,#110513,#110514,#110515,#110516,#110517,
#110518,#110519,#110520,#110521,#110522,#110523,#110524,#110525,#110526,
#110527,#110528,#110529,#110530,#110531,#110532,#110533,#110534,#110535,
#110536,#110537,#110538,#110539,#110540,#110541,#110542,#110543,#110544,
#110545,#110546,#110547,#110548,#110549,#110550,#110551,#110552,#110553,
#110554,#110555)),.UNSPECIFIED.,.F.,.F.,.F.,(4,4),(4,1,1,1,1,1,1,1,1,1,
1,1,1,1,1,1,1,1,1,1,1,1,1,1,1,1,1,1,1,1,1,1,1,1,1,1,1,1,1,1,1,1,1,1,1,1,
1,1,4),(0.,0.0262983047615868),(8.30929135176535,9.30134463307939,10.2933979143934,
11.2854511957075,12.2775044770215,13.2695577583356,14.2616110396496,15.2536643209636,
16.2457176022777,17.2377708835917,18.2298241649058,19.2218774462198,20.2139307275338,
21.2059840088479,22.1980372901619,23.1900905714759,24.18214385279,25.174197134104,
26.1662504154181,27.1583036967321,28.1503569780461,29.1424102593602,30.1344635406742,
31.1265168219883,32.1185701033023,33.1106233846163,34.1026766659304,35.0947299472444,
36.0867832285585,37.0788365098725,38.0708897911865,39.0629430725006,40.0549963538146,
41.0470496351287,42.0391029164427,43.0311561977567,44.0232094790708,45.0152627603848,
46.0073160416989,46.9993693230129,47.9914226043269,48.983475885641,49.975529166955,
50.967582448269,51.9596357295831,52.9516890108971,53.9437422922112,54.9357955735252,
55.9278488548392),.UNSPECIFIED.);
#57122=B_SPLINE_SURFACE_WITH_KNOTS('',3,3,((#110734,#110735,#110736,#110737,
#110738,#110739,#110740,#110741,#110742,#110743,#110744,#110745,#110746,
#110747,#110748,#110749,#110750,#110751,#110752,#110753,#110754,#110755,
#110756,#110757,#110758,#110759,#110760,#110761,#110762,#110763,#110764,
#110765,#110766,#110767,#110768,#110769,#110770,#110771,#110772,#110773,
#110774,#110775,#110776,#110777,#110778,#110779,#110780,#110781,#110782,
#110783,#110784),(#110785,#110786,#110787,#110788,#110789,#110790,#110791,
#110792,#110793,#110794,#110795,#110796,#110797,#110798,#110799,#110800,
#110801,#110802,#110803,#110804,#110805,#110806,#110807,#110808,#110809,
#110810,#110811,#110812,#110813,#110814,#110815,#110816,#110817,#110818,
#110819,#110820,#110821,#110822,#110823,#110824,#110825,#110826,#110827,
#110828,#110829,#110830,#110831,#110832,#110833,#110834,#110835),(#110836,
#110837,#110838,#110839,#110840,#110841,#110842,#110843,#110844,#110845,
#110846,#110847,#110848,#110849,#110850,#110851,#110852,#110853,#110854,
#110855,#110856,#110857,#110858,#110859,#110860,#110861,#110862,#110863,
#110864,#110865,#110866,#110867,#110868,#110869,#110870,#110871,#110872,
#110873,#110874,#110875,#110876,#110877,#110878,#110879,#110880,#110881,
#110882,#110883,#110884,#110885,#110886),(#110887,#110888,#110889,#110890,
#110891,#110892,#110893,#110894,#110895,#110896,#110897,#110898,#110899,
#110900,#110901,#110902,#110903,#110904,#110905,#110906,#110907,#110908,
#110909,#110910,#110911,#110912,#110913,#110914,#110915,#110916,#110917,
#110918,#110919,#110920,#110921,#110922,#110923,#110924,#110925,#110926,
#110927,#110928,#110929,#110930,#110931,#110932,#110933,#110934,#110935,
#110936,#110937)),.UNSPECIFIED.,.F.,.F.,.F.,(4,4),(4,1,1,1,1,1,1,1,1,1,
1,1,1,1,1,1,1,1,1,1,1,1,1,1,1,1,1,1,1,1,1,1,1,1,1,1,1,1,1,1,1,1,1,1,1,1,
1,1,4),(0.,0.0262983047615868),(11.6163931973415,12.6084464786556,13.6004997599696,
14.5925530412836,15.5846063225977,16.5766596039117,17.5687128852257,18.5607661665398,
19.5528194478538,20.5448727291679,21.5369260104819,22.5289792917959,23.52103257311,
24.513085854424,25.5051391357381,26.4971924170521,27.4892456983661,28.4812989796802,
29.4733522609942,30.4654055423083,31.4574588236223,32.4495121049363,33.4415653862504,
34.4336186675644,35.4256719488784,36.4177252301925,37.4097785115065,38.4018317928206,
39.3938850741346,40.3859383554486,41.3779916367627,42.3700449180767,43.3620981993908,
44.3541514807048,45.3462047620188,46.3382580433329,47.3303113246469,48.322364605961,
49.314417887275,50.306471168589,51.2985244499031,52.2905777312171,53.2826310125312,
54.2746842938452,55.2667375751592,56.2587908564733,57.2508441377873,58.2428974191013,
59.2349507004154),.UNSPECIFIED.);
#60182=ADVANCED_FACE('',(#7082),#823,.T.);
#60183=ADVANCED_FACE('',(#7083),#824,.T.);
#60184=ADVANCED_FACE('',(#7084),#825,.T.);
#60185=ADVANCED_FACE('',(#7085),#826,.T.);
#60186=ADVANCED_FACE('',(#7086),#827,.T.);
#60187=ADVANCED_FACE('',(#7087),#828,.T.);
#60188=ADVANCED_FACE('',(#7088),#829,.T.);
#60189=ADVANCED_FACE('',(#7089),#830,.T.);
#60190=ADVANCED_FACE('',(#7090),#831,.T.);
#60191=ADVANCED_FACE('',(#7091),#832,.T.);
#60192=ADVANCED_FACE('',(#7092),#833,.T.);
#60193=ADVANCED_FACE('',(#7093),#834,.T.);
#60194=ADVANCED_FACE('',(#7094),#835,.T.);
#60195=ADVANCED_FACE('',(#7095),#836,.T.);
#60196=ADVANCED_FACE('',(#7096),#837,.T.);
#60197=ADVANCED_FACE('',(#7097),#3881,.F.);
#60198=ADVANCED_FACE('',(#7098),#57121,.F.);
#60199=ADVANCED_FACE('',(#7099),#3882,.T.);
#60200=ADVANCED_FACE('',(#7100),#838,.T.);
#60201=ADVANCED_FACE('',(#7101),#57122,.F.);
#60202=ADVANCED_FACE('',(#7102),#3883,.F.);
#60203=ADVANCED_FACE('',(#7103),#3884,.F.);
#60204=ADVANCED_FACE('',(#7104),#3885,.F.);
#60205=ADVANCED_FACE('',(#7105),#3886,.F.);
#60206=ADVANCED_FACE('',(#7106),#3887,.F.);
#60207=ADVANCED_FACE('',(#7107),#3888,.F.);
#60208=ADVANCED_FACE('',(#7108),#3889,.F.);
#60209=ADVANCED_FACE('',(#7109),#3890,.T.);
#60210=ADVANCED_FACE('',(#7110),#949,.T.);
#60211=ADVANCED_FACE('',(#7111),#839,.T.);
#60212=ADVANCED_FACE('',(#7112),#950,.T.);
#60213=ADVANCED_FACE('',(#7113,#1856),#3891,.T.);
#60407=CLOSED_SHELL('',(#60182,#60183,#60184,#60185,#60186,#60187,#60188,
#60189,#60190,#60191,#60192,#60193,#60194,#60195,#60196,#60197,#60198,#60199,
#60200,#60201,#60202,#60203,#60204,#60205,#60206,#60207,#60208,#60209,#60210,
#60211,#60212,#60213));
#63421=AXIS2_PLACEMENT_3D('',#109660,#75156,#75157);
#63422=AXIS2_PLACEMENT_3D('',#109661,#75158,#75159);
#63423=AXIS2_PLACEMENT_3D('',#109677,#75161,#75162);
#63424=AXIS2_PLACEMENT_3D('',#109685,#75163,#75164);
#63425=AXIS2_PLACEMENT_3D('',#109733,#75166,#75167);
#63426=AXIS2_PLACEMENT_3D('',#109781,#75169,#75170);
#63427=AXIS2_PLACEMENT_3D('',#109835,#75172,#75173);
#63428=AXIS2_PLACEMENT_3D('',#109883,#75175,#75176);
#63429=AXIS2_PLACEMENT_3D('',#109931,#75178,#75179);
#63430=AXIS2_PLACEMENT_3D('',#109985,#75181,#75182);
#63431=AXIS2_PLACEMENT_3D('',#109990,#75184,#75185);
#63432=AXIS2_PLACEMENT_3D('',#110032,#75186,#75187);
#63433=AXIS2_PLACEMENT_3D('',#110045,#75189,#75190);
#63434=AXIS2_PLACEMENT_3D('',#110052,#75191,#75192);
#63435=AXIS2_PLACEMENT_3D('',#110077,#75194,#75195);
#63436=AXIS2_PLACEMENT_3D('',#110102,#75197,#75198);
#63437=AXIS2_PLACEMENT_3D('',#110126,#75200,#75201);
#63438=AXIS2_PLACEMENT_3D('',#110151,#75203,#75204);
#63439=AXIS2_PLACEMENT_3D('',#110176,#75206,#75207);
#63440=AXIS2_PLACEMENT_3D('',#110200,#75209,#75210);
#63441=AXIS2_PLACEMENT_3D('',#110275,#75211,#75212);
#63442=AXIS2_PLACEMENT_3D('',#110643,#75213,#75214);
#63443=AXIS2_PLACEMENT_3D('',#110645,#75215,#75216);
#63444=AXIS2_PLACEMENT_3D('',#110646,#75217,#75218);
#63445=AXIS2_PLACEMENT_3D('',#110724,#75219,#75220);
#63446=AXIS2_PLACEMENT_3D('',#110725,#75221,#75222);
#63447=AXIS2_PLACEMENT_3D('',#110938,#75223,#75224);
#63448=AXIS2_PLACEMENT_3D('',#110947,#75229,#75230);
#63449=AXIS2_PLACEMENT_3D('',#110953,#75234,#75235);
#63450=AXIS2_PLACEMENT_3D('',#110959,#75239,#75240);
#63451=AXIS2_PLACEMENT_3D('',#110965,#75244,#75245);
#63452=AXIS2_PLACEMENT_3D('',#110971,#75249,#75250);
#63453=AXIS2_PLACEMENT_3D('',#110974,#75253,#75254);
#63454=AXIS2_PLACEMENT_3D('',#110975,#75255,#75256);
#63455=AXIS2_PLACEMENT_3D('',#110977,#75257,#75258);
#63456=AXIS2_PLACEMENT_3D('',#110978,#75259,#75260);
#63457=AXIS2_PLACEMENT_3D('',#110980,#75262,#75263);
#63458=AXIS2_PLACEMENT_3D('',#110981,#75264,#75265);
#63459=AXIS2_PLACEMENT_3D('',#110982,#75266,#75267);
#63460=AXIS2_PLACEMENT_3D('',#110984,#75268,#75269);
#63461=AXIS2_PLACEMENT_3D('',#110986,#75271,#75272);
#75156=DIRECTION('axis',(0.,0.,1.));
#75157=DIRECTION('refdir',(1.,0.,0.));
#75158=DIRECTION('center_axis',(0.,0.,1.));
#75159=DIRECTION('ref_axis',(1.,0.,0.));
#75160=DIRECTION('',(0.,0.,-1.));
#75161=DIRECTION('center_axis',(0.,0.,1.));
#75162=DIRECTION('ref_axis',(1.,0.,0.));
#75163=DIRECTION('center_axis',(0.,0.,1.));
#75164=DIRECTION('ref_axis',(1.,0.,0.));
#75165=DIRECTION('',(0.,0.,-1.));
#75166=DIRECTION('center_axis',(0.,0.,1.));
#75167=DIRECTION('ref_axis',(1.,0.,0.));
#75168=DIRECTION('',(0.,0.,-1.));
#75169=DIRECTION('center_axis',(0.,0.,1.));
#75170=DIRECTION('ref_axis',(1.,0.,0.));
#75171=DIRECTION('',(0.,0.,-1.));
#75172=DIRECTION('center_axis',(0.,0.,1.));
#75173=DIRECTION('ref_axis',(1.,0.,0.));
#75174=DIRECTION('',(0.,0.,-1.));
#75175=DIRECTION('center_axis',(0.,0.,1.));
#75176=DIRECTION('ref_axis',(1.,0.,0.));
#75177=DIRECTION('',(0.,0.,-1.));
#75178=DIRECTION('center_axis',(0.,0.,1.));
#75179=DIRECTION('ref_axis',(1.,0.,0.));
#75180=DIRECTION('',(0.,0.,-1.));
#75181=DIRECTION('center_axis',(0.,0.,1.));
#75182=DIRECTION('ref_axis',(1.,0.,0.));
#75183=DIRECTION('',(0.,0.,-1.));
#75184=DIRECTION('center_axis',(0.,0.,1.));
#75185=DIRECTION('ref_axis',(1.,0.,0.));
#75186=DIRECTION('center_axis',(0.,0.,1.));
#75187=DIRECTION('ref_axis',(0.305350463707712,-0.95224004028054,0.));
#75188=DIRECTION('',(0.,0.,1.));
#75189=DIRECTION('center_axis',(0.,0.,1.));
#75190=DIRECTION('ref_axis',(1.,2.70419681234815E-14,0.));
#75191=DIRECTION('center_axis',(0.,0.,1.));
#75192=DIRECTION('ref_axis',(1.,2.70419681234815E-14,0.));
#75193=DIRECTION('',(0.,0.,1.));
#75194=DIRECTION('center_axis',(0.,0.,1.));
#75195=DIRECTION('ref_axis',(1.,2.70419681234815E-14,0.));
#75196=DIRECTION('',(0.,0.,1.));
#75197=DIRECTION('center_axis',(0.,0.,1.));
#75198=DIRECTION('ref_axis',(1.,2.70419681234815E-14,0.));
#75199=DIRECTION('',(0.,0.,1.));
#75200=DIRECTION('center_axis',(0.,0.,1.));
#75201=DIRECTION('ref_axis',(1.,2.70419681234815E-14,0.));
#75202=DIRECTION('',(0.,0.,1.));
#75203=DIRECTION('center_axis',(0.,0.,1.));
#75204=DIRECTION('ref_axis',(1.,2.70419681234815E-14,0.));
#75205=DIRECTION('',(0.,0.,1.));
#75206=DIRECTION('center_axis',(0.,0.,1.));
#75207=DIRECTION('ref_axis',(1.,2.70419681234815E-14,0.));
#75208=DIRECTION('',(0.,0.,1.));
#75209=DIRECTION('center_axis',(0.,0.,1.));
#75210=DIRECTION('ref_axis',(1.,0.,0.));
#75211=DIRECTION('center_axis',(0.,0.,1.));
#75212=DIRECTION('ref_axis',(1.,0.,0.));
#75213=DIRECTION('center_axis',(0.,0.,1.));
#75214=DIRECTION('ref_axis',(1.,0.,0.));
#75215=DIRECTION('center_axis',(0.,0.,1.));
#75216=DIRECTION('ref_axis',(1.,0.,0.));
#75217=DIRECTION('center_axis',(0.,0.,1.));
#75218=DIRECTION('ref_axis',(1.,0.,0.));
#75219=DIRECTION('center_axis',(0.,0.,-1.));
#75220=DIRECTION('ref_axis',(1.,2.70419681234815E-14,0.));
#75221=DIRECTION('center_axis',(0.,0.,1.));
#75222=DIRECTION('ref_axis',(1.,2.70419681234815E-14,0.));
#75223=DIRECTION('center_axis',(0.866025403784442,0.499999999999995,0.));
#75224=DIRECTION('ref_axis',(0.499999999999995,-0.866025403784442,0.));
#75225=DIRECTION('',(0.499999999999995,-0.866025403784442,0.));
#75226=DIRECTION('',(0.,0.,-1.));
#75227=DIRECTION('',(0.499999999999995,-0.866025403784442,0.));
#75228=DIRECTION('',(0.,0.,-1.));
#75229=DIRECTION('center_axis',(0.,1.,0.));
#75230=DIRECTION('ref_axis',(1.,0.,0.));
#75231=DIRECTION('',(1.,0.,0.));
#75232=DIRECTION('',(0.,0.,-1.));
#75233=DIRECTION('',(1.,0.,0.));
#75234=DIRECTION('center_axis',(-0.866025403784442,0.499999999999995,0.));
#75235=DIRECTION('ref_axis',(0.499999999999995,0.866025403784442,0.));
#75236=DIRECTION('',(0.499999999999995,0.866025403784442,0.));
#75237=DIRECTION('',(0.,0.,-1.));
#75238=DIRECTION('',(0.499999999999995,0.866025403784442,0.));
#75239=DIRECTION('center_axis',(-0.866025403784442,-0.499999999999993,0.));
#75240=DIRECTION('ref_axis',(-0.499999999999993,0.866025403784442,0.));
#75241=DIRECTION('',(-0.499999999999993,0.866025403784442,0.));
#75242=DIRECTION('',(0.,0.,-1.));
#75243=DIRECTION('',(-0.499999999999993,0.866025403784442,0.));
#75244=DIRECTION('center_axis',(0.,-1.,0.));
#75245=DIRECTION('ref_axis',(-1.,0.,0.));
#75246=DIRECTION('',(-1.,0.,0.));
#75247=DIRECTION('',(0.,0.,-1.));
#75248=DIRECTION('',(-1.,0.,0.));
#75249=DIRECTION('center_axis',(0.866025403784442,-0.499999999999993,0.));
#75250=DIRECTION('ref_axis',(-0.499999999999993,-0.866025403784442,0.));
#75251=DIRECTION('',(-0.499999999999993,-0.866025403784442,0.));
#75252=DIRECTION('',(-0.499999999999993,-0.866025403784442,0.));
#75253=DIRECTION('center_axis',(0.,0.,-1.));
#75254=DIRECTION('ref_axis',(-1.,0.,0.));
#75255=DIRECTION('center_axis',(0.,0.,-1.));
#75256=DIRECTION('ref_axis',(-1.,0.,0.));
#75257=DIRECTION('center_axis',(0.,0.,1.));
#75258=DIRECTION('ref_axis',(1.,0.,0.));
#75259=DIRECTION('center_axis',(0.,0.,1.));
#75260=DIRECTION('ref_axis',(1.,0.,0.));
#75261=DIRECTION('',(0.707106781186532,8.65956056235474E-17,-0.707106781186563));
#75262=DIRECTION('center_axis',(0.,0.,1.));
#75263=DIRECTION('ref_axis',(-0.974166089596959,-0.225832747579639,0.));
#75264=DIRECTION('center_axis',(0.,0.,1.));
#75265=DIRECTION('ref_axis',(1.,0.,0.));
#75266=DIRECTION('center_axis',(0.,0.,1.));
#75267=DIRECTION('ref_axis',(1.,0.,0.));
#75268=DIRECTION('center_axis',(0.,0.,1.));
#75269=DIRECTION('ref_axis',(1.,0.,0.));
#75270=DIRECTION('',(0.707106781186547,8.65956056235493E-17,-0.707106781186547));
#75271=DIRECTION('center_axis',(0.,0.,1.));
#75272=DIRECTION('ref_axis',(1.,0.,0.));
#109660=CARTESIAN_POINT('',(0.,0.,0.));
#109661=CARTESIAN_POINT('Origin',(101.5,10.2,47.3));
#109662=CARTESIAN_POINT('',(100.532241706852,10.2006700084922,45.9457359168897));
#109663=CARTESIAN_POINT('',(100.53250240679,10.200740851054,45.8877640831103));
#109664=CARTESIAN_POINT('',(100.53325,10.2,47.3));
#109665=CARTESIAN_POINT('',(101.925646819763,11.0688404025234,45.81675));
#109666=CARTESIAN_POINT('Ctrl Pts',(100.532241706852,10.2006700084922,45.9457359168897));
#109667=CARTESIAN_POINT('Ctrl Pts',(100.531939678106,10.2403060092119,45.9431182012074));
#109668=CARTESIAN_POINT('Ctrl Pts',(100.534165142082,10.2799067243431,45.940500485525));
#109669=CARTESIAN_POINT('Ctrl Pts',(100.539032731449,10.3191783203179,45.9378827698427));
#109670=CARTESIAN_POINT('Ctrl Pts',(100.578178545175,10.6350058202473,45.9168307453719));
#109671=CARTESIAN_POINT('Ctrl Pts',(100.788206315339,10.9295472277339,45.895778720901));
#109672=CARTESIAN_POINT('Ctrl Pts',(101.074083348808,11.0695984076775,45.8747266964301));
#109673=CARTESIAN_POINT('Ctrl Pts',(101.336515844848,11.1981641069922,45.8554011309534));
#109674=CARTESIAN_POINT('Ctrl Pts',(101.66286705885,11.1965397839927,45.8360755654767));
#109675=CARTESIAN_POINT('Ctrl Pts',(101.926174511012,11.0694185813664,45.81675));
#109676=CARTESIAN_POINT('',(101.074880871485,11.0682622236804,45.81675));
#109677=CARTESIAN_POINT('Origin',(101.5,10.2,45.81675));
#109678=CARTESIAN_POINT('Ctrl Pts',(101.074880871485,11.0682622236804,45.81675));
#109679=CARTESIAN_POINT('Ctrl Pts',(100.78776007547,10.9276819482162,45.8378020244709));
#109680=CARTESIAN_POINT('Ctrl Pts',(100.578312683887,10.6345304198673,45.8588540489418));
#109681=CARTESIAN_POINT('Ctrl Pts',(100.539273609597,10.3191833556862,45.8799060734127));
#109682=CARTESIAN_POINT('Ctrl Pts',(100.534416286971,10.2799472196416,45.8825254099786));
#109683=CARTESIAN_POINT('Ctrl Pts',(100.532197030409,10.2403674777756,45.8851447465444));
#109684=CARTESIAN_POINT('Ctrl Pts',(100.53250240679,10.200740851054,45.8877640831103));
#109685=CARTESIAN_POINT('Origin',(101.5,10.2,47.3));
#109686=CARTESIAN_POINT('',(100.534708414766,10.2002149330439,46.3457359168897));
#109687=CARTESIAN_POINT('',(100.534710545659,10.2002170964104,46.2877640831103));
#109688=CARTESIAN_POINT('',(100.53325,10.2,47.3));
#109689=CARTESIAN_POINT('Ctrl Pts',(100.534708414766,10.2002149330439,46.3457359168897));
#109690=CARTESIAN_POINT('Ctrl Pts',(100.534413669718,10.3471285850105,46.3360970146994));
#109691=CARTESIAN_POINT('Ctrl Pts',(100.565907422062,10.4939222620691,46.3264581125091));
#109692=CARTESIAN_POINT('Ctrl Pts',(100.629847246181,10.624873077704,46.3168192103187));
#109693=CARTESIAN_POINT('Ctrl Pts',(100.769496214025,10.9108786539404,46.2957671858479));
#109694=CARTESIAN_POINT('Ctrl Pts',(101.063918007077,11.1213113090886,46.274715161377));
#109695=CARTESIAN_POINT('Ctrl Pts',(101.379732776824,11.1608420226805,46.2536631369061));
#109696=CARTESIAN_POINT('Ctrl Pts',(101.695547546572,11.2003727362724,46.2326111124352));
#109697=CARTESIAN_POINT('Ctrl Pts',(102.032755293016,11.0690015083081,46.2115590879643));
#109698=CARTESIAN_POINT('Ctrl Pts',(102.238588515748,10.8262372585098,46.1905070634934));
#109699=CARTESIAN_POINT('Ctrl Pts',(102.444421738481,10.5834730087115,46.1694550390225));
#109700=CARTESIAN_POINT('Ctrl Pts',(102.518880437503,10.2293157370793,46.1484030145516));
#109701=CARTESIAN_POINT('Ctrl Pts',(102.42823895665,9.92422086028216,46.1273509900807));
#109702=CARTESIAN_POINT('Ctrl Pts',(102.337597475796,9.61912598348505,46.1062989656099));
#109703=CARTESIAN_POINT('Ctrl Pts',(102.081855815067,9.36309350152309,46.085246941139));
#109704=CARTESIAN_POINT('Ctrl Pts',(101.776859159505,9.27208769655593,46.0641949166681));
#109705=CARTESIAN_POINT('Ctrl Pts',(101.471862503943,9.18108189158877,46.0431428921972));
#109706=CARTESIAN_POINT('Ctrl Pts',(101.117610853547,9.2551027636164,46.0220908677263));
#109707=CARTESIAN_POINT('Ctrl Pts',(100.874616956993,9.46066999581634,46.0010388432554));
#109708=CARTESIAN_POINT('Ctrl Pts',(100.661838156121,9.64067595393337,45.9826045344668));
#109709=CARTESIAN_POINT('Ctrl Pts',(100.534368634238,9.92154791691139,45.9641702256782));
#109710=CARTESIAN_POINT('Ctrl Pts',(100.532241706852,10.2006700084922,45.9457359168897));
#109711=CARTESIAN_POINT('Ctrl Pts',(100.53250240679,10.200740851054,45.8877640831103));
#109712=CARTESIAN_POINT('Ctrl Pts',(100.534651388942,9.92188197793314,45.9061967710153));
#109713=CARTESIAN_POINT('Ctrl Pts',(100.661824251252,9.64070129142659,45.9246294589203));
#109714=CARTESIAN_POINT('Ctrl Pts',(100.874490524577,9.46060350281805,45.9430621468253));
#109715=CARTESIAN_POINT('Ctrl Pts',(101.117377270841,9.25491331414458,45.9641141712962));
#109716=CARTESIAN_POINT('Ctrl Pts',(101.471781520366,9.18107553681112,45.9851661957671));
#109717=CARTESIAN_POINT('Ctrl Pts',(101.776825995409,9.2721133102411,46.006218220238));
#109718=CARTESIAN_POINT('Ctrl Pts',(102.081870470452,9.36315108367107,46.0272702447089));
#109719=CARTESIAN_POINT('Ctrl Pts',(102.337555171014,9.61906440786449,46.0483222691798));
#109720=CARTESIAN_POINT('Ctrl Pts',(102.428200069675,9.92412653627793,46.0693742936507));
#109721=CARTESIAN_POINT('Ctrl Pts',(102.518844968337,10.2291886646914,46.0904263181216));
#109722=CARTESIAN_POINT('Ctrl Pts',(102.444450065097,10.5833995973248,46.1114783425924));
#109723=CARTESIAN_POINT('Ctrl Pts',(102.238644926451,10.8261920261445,46.1325303670633));
#109724=CARTESIAN_POINT('Ctrl Pts',(102.032839787805,11.0689844549642,46.1535823915342));
#109725=CARTESIAN_POINT('Ctrl Pts',(101.695624413753,11.2003583799702,46.1746344160051));
#109726=CARTESIAN_POINT('Ctrl Pts',(101.379802042979,11.1608458039451,46.195686440476));
#109727=CARTESIAN_POINT('Ctrl Pts',(101.063979672205,11.12133322792,46.2167384649469));
#109728=CARTESIAN_POINT('Ctrl Pts',(100.76955030471,10.910934150864,46.2377904894178));
#109729=CARTESIAN_POINT('Ctrl Pts',(100.629881698669,10.6249421244694,46.2588425138887));
#109730=CARTESIAN_POINT('Ctrl Pts',(100.565922129312,10.4939754930551,46.2684830369626));
#109731=CARTESIAN_POINT('Ctrl Pts',(100.534417015093,10.3471564714095,46.2781235600364));
#109732=CARTESIAN_POINT('Ctrl Pts',(100.534710545659,10.2002170964104,46.2877640831103));
#109733=CARTESIAN_POINT('Origin',(101.5,10.2,47.3));
#109734=CARTESIAN_POINT('',(100.532976005802,10.1991590825138,46.7457359168897));
#109735=CARTESIAN_POINT('',(100.532975287323,10.1991591673174,46.6877640831103));
#109736=CARTESIAN_POINT('',(100.53325,10.2,47.3));
#109737=CARTESIAN_POINT('Ctrl Pts',(100.532976005802,10.1991590825138,46.7457359168897));
#109738=CARTESIAN_POINT('Ctrl Pts',(100.535266693318,10.4519363514863,46.7290758281913));
#109739=CARTESIAN_POINT('Ctrl Pts',(100.63701805918,10.7063475805698,46.712415739493));
#109740=CARTESIAN_POINT('Ctrl Pts',(100.815067785654,10.8845077228383,46.6957556507947));
#109741=CARTESIAN_POINT('Ctrl Pts',(101.040055015112,11.1096344759239,46.6747036263238));
#109742=CARTESIAN_POINT('Ctrl Pts',(101.386870582805,11.2130083745455,46.653651601853));
#109743=CARTESIAN_POINT('Ctrl Pts',(101.698397381134,11.1477981944709,46.6325995773821));
#109744=CARTESIAN_POINT('Ctrl Pts',(102.009924179463,11.0825880143963,46.6115475529112));
#109745=CARTESIAN_POINT('Ctrl Pts',(102.286162208427,10.8487937556255,46.5904955284403));
#109746=CARTESIAN_POINT('Ctrl Pts',(102.401967899387,10.5523306652483,46.5694435039694));
#109747=CARTESIAN_POINT('Ctrl Pts',(102.517773590346,10.2558675748711,46.5483914794985));
#109748=CARTESIAN_POINT('Ctrl Pts',(102.473146943299,9.89673565288765,46.5273394550276));
#109749=CARTESIAN_POINT('Ctrl Pts',(102.288305150741,9.63763182842371,46.5062874305567));
#109750=CARTESIAN_POINT('Ctrl Pts',(102.103463358183,9.37852800395976,46.4852354060859));
#109751=CARTESIAN_POINT('Ctrl Pts',(101.778406420114,9.21945227701537,46.464183381615));
#109752=CARTESIAN_POINT('Ctrl Pts',(101.46039403625,9.23247007300103,46.4431313571441));
#109753=CARTESIAN_POINT('Ctrl Pts',(101.142381652385,9.24548786898669,46.4220793326731));
#109754=CARTESIAN_POINT('Ctrl Pts',(100.831413822726,9.43059918790241,46.4010273082023));
#109755=CARTESIAN_POINT('Ctrl Pts',(100.668367979214,9.70394409602264,46.3799752837314));
#109756=CARTESIAN_POINT('Ctrl Pts',(100.579974478061,9.85213501540243,46.3685621614508));
#109757=CARTESIAN_POINT('Ctrl Pts',(100.535057413148,10.0262590777531,46.3571490391703));
#109758=CARTESIAN_POINT('Ctrl Pts',(100.534708414766,10.2002149330439,46.3457359168897));
#109759=CARTESIAN_POINT('Ctrl Pts',(100.534710545659,10.2002170964104,46.2877640831103));
#109760=CARTESIAN_POINT('Ctrl Pts',(100.535057998223,10.0262847412647,46.2991755845073));
#109761=CARTESIAN_POINT('Ctrl Pts',(100.579960096027,9.85218375311567,46.3105870859043));
#109762=CARTESIAN_POINT('Ctrl Pts',(100.668329149821,9.7040063815298,46.3219985873014));
#109763=CARTESIAN_POINT('Ctrl Pts',(100.831353051604,9.43064764071791,46.3430506117722));
#109764=CARTESIAN_POINT('Ctrl Pts',(101.142308699758,9.24551513482726,46.3641026362431));
#109765=CARTESIAN_POINT('Ctrl Pts',(101.460320593408,9.23247371374772,46.385154660714));
#109766=CARTESIAN_POINT('Ctrl Pts',(101.778332487057,9.21943229266818,46.4062066851849));
#109767=CARTESIAN_POINT('Ctrl Pts',(102.103400626201,9.37848195639975,46.4272587096558));
#109768=CARTESIAN_POINT('Ctrl Pts',(102.288261961448,9.63757133787734,46.4483107341267));
#109769=CARTESIAN_POINT('Ctrl Pts',(102.473123296695,9.89666071935493,46.4693627585976));
#109770=CARTESIAN_POINT('Ctrl Pts',(102.517777828044,10.2557898185785,46.4904147830684));
#109771=CARTESIAN_POINT('Ctrl Pts',(102.401994901457,10.5522619030281,46.5114668075393));
#109772=CARTESIAN_POINT('Ctrl Pts',(102.28621197487,10.8487339874777,46.5325188320102));
#109773=CARTESIAN_POINT('Ctrl Pts',(102.009991590346,11.0825490571533,46.5535708564811));
#109774=CARTESIAN_POINT('Ctrl Pts',(101.698469721739,11.1477829573153,46.574622880952));
#109775=CARTESIAN_POINT('Ctrl Pts',(101.386947853131,11.2130168574774,46.5956749054229));
#109776=CARTESIAN_POINT('Ctrl Pts',(101.040124500441,11.109669588126,46.6167269298938));
#109777=CARTESIAN_POINT('Ctrl Pts',(100.815120106439,10.8845600595657,46.6377789543647));
#109778=CARTESIAN_POINT('Ctrl Pts',(100.637039472308,10.7063962162653,46.6544406639466));
#109779=CARTESIAN_POINT('Ctrl Pts',(100.535266170519,10.4519605571488,46.6711023735285));
#109780=CARTESIAN_POINT('Ctrl Pts',(100.532975287323,10.1991591673174,46.6877640831103));
#109781=CARTESIAN_POINT('Origin',(101.5,10.2,47.3));
#109782=CARTESIAN_POINT('',(100.532227115867,10.2006344259866,47.1457359168897));
#109783=CARTESIAN_POINT('',(100.532227739394,10.2006347153061,47.0877640831103));
#109784=CARTESIAN_POINT('',(100.53325,10.2,47.3));
#109785=CARTESIAN_POINT('Ctrl Pts',(100.532227115867,10.2006344259866,47.1457359168897));
#109786=CARTESIAN_POINT('Ctrl Pts',(100.531923761155,10.2404469978614,47.1431066661542));
#109787=CARTESIAN_POINT('Ctrl Pts',(100.53417029479,10.2802250774012,47.1404774154188));
#109788=CARTESIAN_POINT('Ctrl Pts',(100.539082845792,10.3196711352656,47.1378481646834));
#109789=CARTESIAN_POINT('Ctrl Pts',(100.578416920137,10.6355099269982,47.1167961402125));
#109790=CARTESIAN_POINT('Ctrl Pts',(100.788668560015,10.930062909731,47.0957441157416));
#109791=CARTESIAN_POINT('Ctrl Pts',(101.07458790823,11.0698893665793,47.0746920912707));
#109792=CARTESIAN_POINT('Ctrl Pts',(101.360507256445,11.2097158234276,47.0536400667998));
#109793=CARTESIAN_POINT('Ctrl Pts',(101.722094312998,11.1948157543913,47.032588042329));
#109794=CARTESIAN_POINT('Ctrl Pts',(101.995540056344,11.0319393067675,47.0115360178581));
#109795=CARTESIAN_POINT('Ctrl Pts',(102.268985799689,10.8690628591437,46.9904839933872));
#109796=CARTESIAN_POINT('Ctrl Pts',(102.454290229828,10.5582100329325,46.9694319689163));
#109797=CARTESIAN_POINT('Ctrl Pts',(102.467505271055,10.2402058276111,46.9483799444454));
#109798=CARTESIAN_POINT('Ctrl Pts',(102.480720312281,9.92220162228974,46.9273279199745));
#109799=CARTESIAN_POINT('Ctrl Pts',(102.321845964596,9.59704603785827,46.9062758955036));
#109800=CARTESIAN_POINT('Ctrl Pts',(102.06285673967,9.41204362497134,46.8852238710327));
#109801=CARTESIAN_POINT('Ctrl Pts',(101.803867514744,9.22704121208441,46.8641718465618));
#109802=CARTESIAN_POINT('Ctrl Pts',(101.444763412578,9.18219197074201,46.843119822091));
#109803=CARTESIAN_POINT('Ctrl Pts',(101.148228605385,9.29781385427975,46.8220677976201));
#109804=CARTESIAN_POINT('Ctrl Pts',(100.851693798192,9.41343573781747,46.8010157731492));
#109805=CARTESIAN_POINT('Ctrl Pts',(100.617728285971,9.68952874623533,46.7799637486783));
#109806=CARTESIAN_POINT('Ctrl Pts',(100.552324975472,10.0010150542191,46.7589117242074));
#109807=CARTESIAN_POINT('Ctrl Pts',(100.53868034289,10.0659982514689,46.7545197884348));
#109808=CARTESIAN_POINT('Ctrl Pts',(100.532372134321,10.1325218904679,46.7501278526622));
#109809=CARTESIAN_POINT('Ctrl Pts',(100.532976005802,10.1991590825138,46.7457359168897));
#109810=CARTESIAN_POINT('Ctrl Pts',(100.532975287323,10.1991591673174,46.6877640831103));
#109811=CARTESIAN_POINT('Ctrl Pts',(100.532371645869,10.1325466927522,46.6921543979993));
#109812=CARTESIAN_POINT('Ctrl Pts',(100.538675149134,10.0660476868242,46.6965447128883));
#109813=CARTESIAN_POINT('Ctrl Pts',(100.552309781337,10.0010874279596,46.7009350277773));
#109814=CARTESIAN_POINT('Ctrl Pts',(100.617689285549,9.68959611268303,46.7219870522482));
#109815=CARTESIAN_POINT('Ctrl Pts',(100.851633729287,9.41348526989917,46.7430390767191));
#109816=CARTESIAN_POINT('Ctrl Pts',(101.148159706116,9.29784074657613,46.76409110119));
#109817=CARTESIAN_POINT('Ctrl Pts',(101.444685682945,9.18219622325309,46.7851431256609));
#109818=CARTESIAN_POINT('Ctrl Pts',(101.803793192865,9.22701801939087,46.8061951501318));
#109819=CARTESIAN_POINT('Ctrl Pts',(102.06279654115,9.41200064288986,46.8272471746027));
#109820=CARTESIAN_POINT('Ctrl Pts',(102.321799889436,9.59698326638885,46.8482991990735));
#109821=CARTESIAN_POINT('Ctrl Pts',(102.480699076088,9.92212671724905,46.8693512235444));
#109822=CARTESIAN_POINT('Ctrl Pts',(102.467508326452,10.2401319283015,46.8904032480153));
#109823=CARTESIAN_POINT('Ctrl Pts',(102.454317576816,10.558137139354,46.9114552724862));
#109824=CARTESIAN_POINT('Ctrl Pts',(102.269036890894,10.8690041105988,46.9325072969571));
#109825=CARTESIAN_POINT('Ctrl Pts',(101.995603592515,11.0319014408845,46.953559321428));
#109826=CARTESIAN_POINT('Ctrl Pts',(101.722170294136,11.1947987711702,46.9746113458989));
#109827=CARTESIAN_POINT('Ctrl Pts',(101.360584383302,11.2097264604968,46.9956633703698));
#109828=CARTESIAN_POINT('Ctrl Pts',(101.074654360156,11.0699218457237,47.0167153948407));
#109829=CARTESIAN_POINT('Ctrl Pts',(100.78872433701,10.9301172309506,47.0377674193116));
#109830=CARTESIAN_POINT('Ctrl Pts',(100.578450201553,10.6355803120778,47.0588194437824));
#109831=CARTESIAN_POINT('Ctrl Pts',(100.539092003223,10.3197445300842,47.0798714682533));
#109832=CARTESIAN_POINT('Ctrl Pts',(100.534173408952,10.280274530595,47.0825023398723));
#109833=CARTESIAN_POINT('Ctrl Pts',(100.531924094728,10.2404718960613,47.0851332114913));
#109834=CARTESIAN_POINT('Ctrl Pts',(100.532227739394,10.2006347153061,47.0877640831103));
#109835=CARTESIAN_POINT('Origin',(101.5,10.2,47.3));
#109836=CARTESIAN_POINT('',(100.534709402463,10.2002118426407,47.5457359168897));
#109837=CARTESIAN_POINT('',(100.534709578762,10.2002114578675,47.4877640831103));
#109838=CARTESIAN_POINT('',(100.53325,10.2,47.3));
#109839=CARTESIAN_POINT('Ctrl Pts',(100.534709402463,10.2002118426407,47.5457359168897));
#109840=CARTESIAN_POINT('Ctrl Pts',(100.534418016928,10.3473016191035,47.5360854796462));
#109841=CARTESIAN_POINT('Ctrl Pts',(100.565990448616,10.4942727514434,47.5264350424028));
#109842=CARTESIAN_POINT('Ctrl Pts',(100.630078141595,10.6253456460443,47.5167846051594));
#109843=CARTESIAN_POINT('Ctrl Pts',(100.769882758406,10.9112756733585,47.4957325806885));
#109844=CARTESIAN_POINT('Ctrl Pts',(101.064419681572,11.1215498118811,47.4746805562176));
#109845=CARTESIAN_POINT('Ctrl Pts',(101.38025546817,11.1609080107844,47.4536285317467));
#109846=CARTESIAN_POINT('Ctrl Pts',(101.696091254768,11.2002662096876,47.4325765072758));
#109847=CARTESIAN_POINT('Ctrl Pts',(102.033225904797,11.0687084689717,47.4115244828049));
#109848=CARTESIAN_POINT('Ctrl Pts',(102.238928019467,10.8258341151079,47.390472458334));
#109849=CARTESIAN_POINT('Ctrl Pts',(102.444630134137,10.5829597612441,47.3694204338631));
#109850=CARTESIAN_POINT('Ctrl Pts',(102.518899713447,10.2287687942324,47.3483684093923));
#109851=CARTESIAN_POINT('Ctrl Pts',(102.428090566094,9.92371960069865,47.3273163849214));
#109852=CARTESIAN_POINT('Ctrl Pts',(102.337281418742,9.61867040716488,47.3062643604505));
#109853=CARTESIAN_POINT('Ctrl Pts',(102.081393544726,9.36276298710905,47.2852123359796));
#109854=CARTESIAN_POINT('Ctrl Pts',(101.776351288236,9.27193053958364,47.2641603115087));
#109855=CARTESIAN_POINT('Ctrl Pts',(101.471309031746,9.18109809205824,47.2431082870378));
#109856=CARTESIAN_POINT('Ctrl Pts',(101.117112392783,9.25534061706326,47.222056262567));
#109857=CARTESIAN_POINT('Ctrl Pts',(100.874222327708,9.46102417993194,47.2010042380961));
#109858=CARTESIAN_POINT('Ctrl Pts',(100.661667534337,9.64101930320724,47.1825814643606));
#109859=CARTESIAN_POINT('Ctrl Pts',(100.534352677778,9.92167358227858,47.1641586906251));
#109860=CARTESIAN_POINT('Ctrl Pts',(100.532227115867,10.2006344259866,47.1457359168897));
#109861=CARTESIAN_POINT('Ctrl Pts',(100.532227739394,10.2006347153061,47.0877640831103));
#109862=CARTESIAN_POINT('Ctrl Pts',(100.53435383508,9.92169795891722,47.1061852359622));
#109863=CARTESIAN_POINT('Ctrl Pts',(100.661643552647,9.64106750889965,47.1246063888141));
#109864=CARTESIAN_POINT('Ctrl Pts',(100.874165894016,9.46107199130515,47.143027541666));
#109865=CARTESIAN_POINT('Ctrl Pts',(101.117040244339,9.25536987963401,47.1640795661369));
#109866=CARTESIAN_POINT('Ctrl Pts',(101.471231206187,9.18110030140608,47.1851315906077));
#109867=CARTESIAN_POINT('Ctrl Pts',(101.776280395274,9.27190944743508,47.2061836150786));
#109868=CARTESIAN_POINT('Ctrl Pts',(102.081329584361,9.36271859346409,47.2272356395495));
#109869=CARTESIAN_POINT('Ctrl Pts',(102.337237000686,9.61860646375003,47.2482876640204));
#109870=CARTESIAN_POINT('Ctrl Pts',(102.428069446887,9.92364871579281,47.2693396884913));
#109871=CARTESIAN_POINT('Ctrl Pts',(102.518901893088,10.2286909678356,47.2903917129622));
#109872=CARTESIAN_POINT('Ctrl Pts',(102.444659369166,10.5828876016352,47.3114437374331));
#109873=CARTESIAN_POINT('Ctrl Pts',(102.238975809295,10.8257776631693,47.332495761904));
#109874=CARTESIAN_POINT('Ctrl Pts',(102.033292249425,11.0686677247035,47.3535477863749));
#109875=CARTESIAN_POINT('Ctrl Pts',(101.696167653607,11.2002512139721,47.3745998108458));
#109876=CARTESIAN_POINT('Ctrl Pts',(101.380328866479,11.1609171402,47.3956518353167));
#109877=CARTESIAN_POINT('Ctrl Pts',(101.06449007935,11.1215830664279,47.4167038597875));
#109878=CARTESIAN_POINT('Ctrl Pts',(100.769937100912,10.9113314296151,47.4377558842584));
#109879=CARTESIAN_POINT('Ctrl Pts',(100.630110646102,10.625412085568,47.4588079087293));
#109880=CARTESIAN_POINT('Ctrl Pts',(100.566002176563,10.4943220741444,47.4684599668563));
#109881=CARTESIAN_POINT('Ctrl Pts',(100.534418676151,10.3473259996625,47.4781120249833));
#109882=CARTESIAN_POINT('Ctrl Pts',(100.534709578762,10.2002114578675,47.4877640831103));
#109883=CARTESIAN_POINT('Origin',(101.5,10.2,47.3));
#109884=CARTESIAN_POINT('',(100.532970891558,10.1991597617674,47.9457359168897));
#109885=CARTESIAN_POINT('',(100.532970084924,10.1991597801972,47.8877640831103));
#109886=CARTESIAN_POINT('',(100.53325,10.2,47.3));
#109887=CARTESIAN_POINT('Ctrl Pts',(100.532970891558,10.1991597617674,47.9457359168897));
#109888=CARTESIAN_POINT('Ctrl Pts',(100.535262825522,10.4521085341167,47.9290642931383));
#109889=CARTESIAN_POINT('Ctrl Pts',(100.637170072234,10.7066933040064,47.9123926693868));
#109890=CARTESIAN_POINT('Ctrl Pts',(100.815439930465,10.8848799035489,47.8957210456354));
#109891=CARTESIAN_POINT('Ctrl Pts',(101.040549462316,11.1098843008339,47.8746690211645));
#109892=CARTESIAN_POINT('Ctrl Pts',(101.387421255122,11.2130697376435,47.8536169966936));
#109893=CARTESIAN_POINT('Ctrl Pts',(101.698912574935,11.1476902324763,47.8325649722227));
#109894=CARTESIAN_POINT('Ctrl Pts',(102.010403894747,11.0823107273092,47.8115129477518));
#109895=CARTESIAN_POINT('Ctrl Pts',(102.286514741566,10.8483662801652,47.7904609232809));
#109896=CARTESIAN_POINT('Ctrl Pts',(102.402159266578,10.5518402990146,47.76940889881));
#109897=CARTESIAN_POINT('Ctrl Pts',(102.517803791589,10.255314317864,47.7483568743392));
#109898=CARTESIAN_POINT('Ctrl Pts',(102.472981994793,9.89620680270677,47.7273048498683));
#109899=CARTESIAN_POINT('Ctrl Pts',(102.287999368596,9.63720345064479,47.7062528253974));
#109900=CARTESIAN_POINT('Ctrl Pts',(102.103016742399,9.37820009858282,47.6852008009265));
#109901=CARTESIAN_POINT('Ctrl Pts',(101.777873286802,9.21930090961613,47.6641487764556));
#109902=CARTESIAN_POINT('Ctrl Pts',(101.459868071114,9.23249165944427,47.6430967519847));
#109903=CARTESIAN_POINT('Ctrl Pts',(101.141862855427,9.24568240927242,47.6220447275138));
#109904=CARTESIAN_POINT('Ctrl Pts',(100.830995879649,9.43096309789541,47.6009927030429));
#109905=CARTESIAN_POINT('Ctrl Pts',(100.668098546988,9.70439640025984,47.579940678572));
#109906=CARTESIAN_POINT('Ctrl Pts',(100.579874815821,9.85248541906702,47.5685390913446));
#109907=CARTESIAN_POINT('Ctrl Pts',(100.535053662261,10.0264314351521,47.5571375041171));
#109908=CARTESIAN_POINT('Ctrl Pts',(100.534709402463,10.2002118426407,47.5457359168897));
#109909=CARTESIAN_POINT('Ctrl Pts',(100.534709578762,10.2002114578675,47.4877640831103));
#109910=CARTESIAN_POINT('Ctrl Pts',(100.53505316144,10.0264556844261,47.4991640494542));
#109911=CARTESIAN_POINT('Ctrl Pts',(100.579860827167,9.85253465171874,47.5105640157981));
#109912=CARTESIAN_POINT('Ctrl Pts',(100.668060705361,9.70445995088001,47.521963982142));
#109913=CARTESIAN_POINT('Ctrl Pts',(100.83093715061,9.43101421152056,47.5430160066129));
#109914=CARTESIAN_POINT('Ctrl Pts',(101.14178997229,9.24570978408305,47.5640680310838));
#109915=CARTESIAN_POINT('Ctrl Pts',(101.459794172975,9.23249474304927,47.5851200555547));
#109916=CARTESIAN_POINT('Ctrl Pts',(101.777798373661,9.21927970201549,47.6061720800255));
#109917=CARTESIAN_POINT('Ctrl Pts',(102.102953953352,9.37815404738542,47.6272241044964));
#109918=CARTESIAN_POINT('Ctrl Pts',(102.287956363542,9.63714326853569,47.6482761289673));
#109919=CARTESIAN_POINT('Ctrl Pts',(102.472958773732,9.89613248968595,47.6693281534382));
#109920=CARTESIAN_POINT('Ctrl Pts',(102.51780801442,10.2552365866165,47.6903801779091));
#109921=CARTESIAN_POINT('Ctrl Pts',(102.402186132568,10.5517713894869,47.71143220238));
#109922=CARTESIAN_POINT('Ctrl Pts',(102.286564250716,10.8483061923574,47.7324842268509));
#109923=CARTESIAN_POINT('Ctrl Pts',(102.010471246324,11.0822717011676,47.7535362513218));
#109924=CARTESIAN_POINT('Ctrl Pts',(101.698984942881,11.1476750107129,47.7745882757927));
#109925=CARTESIAN_POINT('Ctrl Pts',(101.387498639437,11.2130783202582,47.7956403002635));
#109926=CARTESIAN_POINT('Ctrl Pts',(101.040619036941,11.1099194305386,47.8166923247344));
#109927=CARTESIAN_POINT('Ctrl Pts',(100.815492287139,10.8849322043608,47.8377443492053));
#109928=CARTESIAN_POINT('Ctrl Pts',(100.637191460131,10.7067418803375,47.8544175938403));
#109929=CARTESIAN_POINT('Ctrl Pts',(100.535262192443,10.4521326485129,47.8710908384753));
#109930=CARTESIAN_POINT('Ctrl Pts',(100.532970084924,10.1991597801972,47.8877640831103));
#109931=CARTESIAN_POINT('Origin',(101.5,10.2,47.3));
#109932=CARTESIAN_POINT('',(100.532234232858,10.2006385183977,48.3457359168897));
#109933=CARTESIAN_POINT('',(100.532232424901,10.200636943667,48.2877640831103));
#109934=CARTESIAN_POINT('',(100.53325,10.2,47.3));
#109935=CARTESIAN_POINT('Ctrl Pts',(100.532234232858,10.2006385183977,48.3457359168897));
#109936=CARTESIAN_POINT('Ctrl Pts',(100.531930164216,10.240627217705,48.3430951311011));
#109937=CARTESIAN_POINT('Ctrl Pts',(100.534197686292,10.2805809022053,48.3404543453126));
#109938=CARTESIAN_POINT('Ctrl Pts',(100.539154181029,10.3201979585981,48.337813559524));
#109939=CARTESIAN_POINT('Ctrl Pts',(100.578666756778,10.6360203339923,48.3167615350531));
#109940=CARTESIAN_POINT('Ctrl Pts',(100.789065838849,10.930449706025,48.2957095105822));
#109941=CARTESIAN_POINT('Ctrl Pts',(101.075057869872,11.0701183141324,48.2746574861114));
#109942=CARTESIAN_POINT('Ctrl Pts',(101.361049900895,11.2097869222398,48.2536054616405));
#109943=CARTESIAN_POINT('Ctrl Pts',(101.722634880869,11.1946947664218,48.2325534371696));
#109944=CARTESIAN_POINT('Ctrl Pts',(101.995993625421,11.0316708622305,48.2115014126987));
#109945=CARTESIAN_POINT('Ctrl Pts',(102.269352369973,10.8686469580393,48.1904493882278));
#109946=CARTESIAN_POINT('Ctrl Pts',(102.454484879102,10.5576913054748,48.1693973637569));
#109947=CARTESIAN_POINT('Ctrl Pts',(102.467526300502,10.2396794072135,48.148345339286));
#109948=CARTESIAN_POINT('Ctrl Pts',(102.480567721901,9.92166750895226,48.1272933148151));
#109949=CARTESIAN_POINT('Ctrl Pts',(102.321518055569,9.59659936499427,48.1062412903442));
#109950=CARTESIAN_POINT('Ctrl Pts',(102.062428670247,9.41173802703683,48.0851892658734));
#109951=CARTESIAN_POINT('Ctrl Pts',(101.803339284925,9.22687668907938,48.0641372414025));
#109952=CARTESIAN_POINT('Ctrl Pts',(101.444210180611,9.18222215712248,48.0430852169316));
#109953=CARTESIAN_POINT('Ctrl Pts',(101.147738091875,9.29800508540701,48.0220331924607));
#109954=CARTESIAN_POINT('Ctrl Pts',(100.851266003139,9.41378801369153,48.0009811679898));
#109955=CARTESIAN_POINT('Ctrl Pts',(100.61745092998,9.69000840221748,47.9799291435189));
#109956=CARTESIAN_POINT('Ctrl Pts',(100.552217028849,10.0015302753606,47.958877119048));
#109957=CARTESIAN_POINT('Ctrl Pts',(100.538643482616,10.0663501998827,47.9544967183286));
#109958=CARTESIAN_POINT('Ctrl Pts',(100.532368695315,10.132698509948,47.9501163176091));
#109959=CARTESIAN_POINT('Ctrl Pts',(100.532970891558,10.1991597617674,47.9457359168897));
#109960=CARTESIAN_POINT('Ctrl Pts',(100.532970084924,10.1991597801972,47.8877640831103));
#109961=CARTESIAN_POINT('Ctrl Pts',(100.532368124453,10.1327232515517,47.8921428629462));
#109962=CARTESIAN_POINT('Ctrl Pts',(100.538638229879,10.0663995843913,47.8965216427821));
#109963=CARTESIAN_POINT('Ctrl Pts',(100.552201819349,10.0016026217589,47.900900422618));
#109964=CARTESIAN_POINT('Ctrl Pts',(100.61741199847,9.69007582797088,47.9219524470889));
#109965=CARTESIAN_POINT('Ctrl Pts',(100.851206253822,9.41383780303078,47.9430044715598));
#109966=CARTESIAN_POINT('Ctrl Pts',(101.147669339883,9.29803211376081,47.9640564960307));
#109967=CARTESIAN_POINT('Ctrl Pts',(101.444132425943,9.18222642449083,47.9851085205015));
#109968=CARTESIAN_POINT('Ctrl Pts',(101.803264342712,9.22685307089099,48.0061605449724));
#109969=CARTESIAN_POINT('Ctrl Pts',(102.062368163389,9.41169486075286,48.0272125694433));
#109970=CARTESIAN_POINT('Ctrl Pts',(102.321471984066,9.59653665061473,48.0482645939142));
#109971=CARTESIAN_POINT('Ctrl Pts',(102.480547708651,9.92159358393832,48.0693166183851));
#109972=CARTESIAN_POINT('Ctrl Pts',(102.467529912874,10.2396059631692,48.090368642856));
#109973=CARTESIAN_POINT('Ctrl Pts',(102.454512117097,10.5576183424,48.1114206673269));
#109974=CARTESIAN_POINT('Ctrl Pts',(102.269400800958,10.8685861675381,48.1324726917977));
#109975=CARTESIAN_POINT('Ctrl Pts',(101.996055896786,11.0316320086696,48.1535247162686));
#109976=CARTESIAN_POINT('Ctrl Pts',(101.722710992614,11.194677849801,48.1745767407395));
#109977=CARTESIAN_POINT('Ctrl Pts',(101.361132500409,11.2098017069258,48.1956287652104));
#109978=CARTESIAN_POINT('Ctrl Pts',(101.075126928412,11.0701527411221,48.2166807896813));
#109979=CARTESIAN_POINT('Ctrl Pts',(100.789121356414,10.9305037753184,48.2377328141522));
#109980=CARTESIAN_POINT('Ctrl Pts',(100.578688704624,10.6360819865862,48.2587848386231));
#109981=CARTESIAN_POINT('Ctrl Pts',(100.539157991476,10.3202672214402,48.279836863094));
#109982=CARTESIAN_POINT('Ctrl Pts',(100.534196177931,10.2806268037821,48.2824792697661));
#109983=CARTESIAN_POINT('Ctrl Pts',(100.531926882114,10.2406493450774,48.2851216764382));
#109984=CARTESIAN_POINT('Ctrl Pts',(100.532232424901,10.200636943667,48.2877640831103));
#109985=CARTESIAN_POINT('Origin',(101.5,10.2,47.3));
#109986=CARTESIAN_POINT('',(100.53325,10.2,48.71675));
#109987=CARTESIAN_POINT('',(100.534608987464,10.2001621159456,48.6877640831103));
#109988=CARTESIAN_POINT('',(100.53325,10.2,47.3));
#109989=CARTESIAN_POINT('',(100.631737776319,10.6251191285149,48.71675));
#109990=CARTESIAN_POINT('Origin',(101.5,10.2,48.71675));
#109991=CARTESIAN_POINT('Ctrl Pts',(100.631737776319,10.625119128515,48.71675));
#109992=CARTESIAN_POINT('Ctrl Pts',(100.772318051784,10.9122399245294,48.6956979755291));
#109993=CARTESIAN_POINT('Ctrl Pts',(101.065469648493,11.1216872926406,48.6746459510583));
#109994=CARTESIAN_POINT('Ctrl Pts',(101.38081672032,11.1607263666344,48.6535939265874));
#109995=CARTESIAN_POINT('Ctrl Pts',(101.696163792148,11.1997654406282,48.6325419021165));
#109996=CARTESIAN_POINT('Ctrl Pts',(102.033706339093,11.0683962205045,48.6114898776456));
#109997=CARTESIAN_POINT('Ctrl Pts',(102.239396511758,10.8255094805151,48.5904378531747));
#109998=CARTESIAN_POINT('Ctrl Pts',(102.445086684422,10.5826227405256,48.5693858287038));
#109999=CARTESIAN_POINT('Ctrl Pts',(102.518924482807,10.2282184806705,48.5483338042329));
#110000=CARTESIAN_POINT('Ctrl Pts',(102.427886711744,9.92317399947378,48.527281779762));
#110001=CARTESIAN_POINT('Ctrl Pts',(102.33684894068,9.61812951827702,48.5062297552911));
#110002=CARTESIAN_POINT('Ctrl Pts',(102.080935600168,9.36244481573861,48.4851777308203));
#110003=CARTESIAN_POINT('Ctrl Pts',(101.775873464374,9.2717999165515,48.4641257063494));
#110004=CARTESIAN_POINT('Ctrl Pts',(101.47081132858,9.18115501736439,48.4430736818785));
#110005=CARTESIAN_POINT('Ctrl Pts',(101.116600397504,9.25554992152858,48.4220216574076));
#110006=CARTESIAN_POINT('Ctrl Pts',(100.873807966679,9.46135506298848,48.4009696329367));
#110007=CARTESIAN_POINT('Ctrl Pts',(100.661471647179,9.64134381355782,48.3825583942544));
#110008=CARTESIAN_POINT('Ctrl Pts',(100.534354162604,9.92184215000783,48.364147155572));
#110009=CARTESIAN_POINT('Ctrl Pts',(100.532234232858,10.2006385183977,48.3457359168897));
#110010=CARTESIAN_POINT('Ctrl Pts',(100.532232424901,10.200636943667,48.2877640831103));
#110011=CARTESIAN_POINT('Ctrl Pts',(100.534361138091,9.92187098952785,48.3061737009091));
#110012=CARTESIAN_POINT('Ctrl Pts',(100.661469771119,9.64140895371578,48.3245833187079));
#110013=CARTESIAN_POINT('Ctrl Pts',(100.873762750332,9.46141149499328,48.3429929365066));
#110014=CARTESIAN_POINT('Ctrl Pts',(101.116526996838,9.25557827525217,48.3640449609775));
#110015=CARTESIAN_POINT('Ctrl Pts',(101.470684264354,9.18111957732977,48.3850969854484));
#110016=CARTESIAN_POINT('Ctrl Pts',(101.775779136246,9.27176105690851,48.4061490099193));
#110017=CARTESIAN_POINT('Ctrl Pts',(102.080874008138,9.36240253648726,48.4272010343902));
#110018=CARTESIAN_POINT('Ctrl Pts',(102.336906484406,9.61814419356716,48.4482530588611));
#110019=CARTESIAN_POINT('Ctrl Pts',(102.427912288884,9.92314084452664,48.469305083332));
#110020=CARTESIAN_POINT('Ctrl Pts',(102.518918093362,10.2281374954861,48.4903571078029));
#110021=CARTESIAN_POINT('Ctrl Pts',(102.444897226051,10.5823891403252,48.5114091322738));
#110022=CARTESIAN_POINT('Ctrl Pts',(102.239329995365,10.8253830337739,48.5324611567446));
#110023=CARTESIAN_POINT('Ctrl Pts',(102.033762764679,11.0683769272226,48.5535131812155));
#110024=CARTESIAN_POINT('Ctrl Pts',(101.696649170618,11.2001130692809,48.5745652056864));
#110025=CARTESIAN_POINT('Ctrl Pts',(101.380821678055,11.1609672548583,48.5956172301573));
#110026=CARTESIAN_POINT('Ctrl Pts',(101.064994185492,11.1218214404357,48.6166692546282));
#110027=CARTESIAN_POINT('Ctrl Pts',(100.770452794427,10.9117936695321,48.6377212790991));
#110028=CARTESIAN_POINT('Ctrl Pts',(100.630401613163,10.625916642522,48.65877330357));
#110029=CARTESIAN_POINT('Ctrl Pts',(100.566113371337,10.4946893920317,48.6684368967501));
#110030=CARTESIAN_POINT('Ctrl Pts',(100.534378091261,10.3474797829438,48.6781004899302));
#110031=CARTESIAN_POINT('Ctrl Pts',(100.534608987464,10.2001621159456,48.6877640831103));
#110032=CARTESIAN_POINT('Origin',(101.5,10.2,45.0772274406976));
#110033=CARTESIAN_POINT('',(100.76022353047,10.200488094229,48.4772274406976));
#110034=CARTESIAN_POINT('',(100.762038832931,10.2001239241621,48.5562725593024));
#110035=CARTESIAN_POINT('',(100.761,10.2,45.0772274406976));
#110036=CARTESIAN_POINT('',(102.101843294079,10.6308187385845,48.71675));
#110037=CARTESIAN_POINT('Ctrl Pts',(100.76022353047,10.200488094229,48.4772274406976));
#110038=CARTESIAN_POINT('Ctrl Pts',(100.761844040511,9.98737144955342,48.49563867938));
#110039=CARTESIAN_POINT('Ctrl Pts',(100.970123064239,9.52778148937982,48.5351019425332));
#110040=CARTESIAN_POINT('Ctrl Pts',(101.748452495356,9.36430899783289,48.5956172301573));
#110041=CARTESIAN_POINT('Ctrl Pts',(102.319282912332,9.93462942377178,48.6570468445758));
#110042=CARTESIAN_POINT('Ctrl Pts',(102.23085022002,10.4483024050457,48.6974244345233));
#110043=CARTESIAN_POINT('Ctrl Pts',(102.101843294079,10.6308187385845,48.71675));
#110044=CARTESIAN_POINT('',(102.101104350279,9.77012262204777,48.71675));
#110045=CARTESIAN_POINT('Origin',(101.5,10.2,48.71675));
#110046=CARTESIAN_POINT('Ctrl Pts',(100.762038832931,10.2001239241621,48.5562725593024));
#110047=CARTESIAN_POINT('Ctrl Pts',(100.762246837233,10.0674118742565,48.5676609905932));
#110048=CARTESIAN_POINT('Ctrl Pts',(100.859509971121,9.68904888221577,48.6001014463548));
#110049=CARTESIAN_POINT('Ctrl Pts',(101.464139111132,9.32935204372765,48.6535939265874));
#110050=CARTESIAN_POINT('Ctrl Pts',(101.958950595826,9.57134677434548,48.6956979755291));
#110051=CARTESIAN_POINT('Ctrl Pts',(102.101104350279,9.77012262204778,48.71675));
#110052=CARTESIAN_POINT('Origin',(101.5,10.2,45.0772274406976));
#110053=CARTESIAN_POINT('',(100.760786644801,10.199357707728,48.0772274406976));
#110054=CARTESIAN_POINT('',(100.760222148438,10.2004868904783,48.1562725593024));
#110055=CARTESIAN_POINT('',(100.761,10.2,45.0772274406976));
#110056=CARTESIAN_POINT('Ctrl Pts',(100.760786644801,10.199357707728,48.0772274406976));
#110057=CARTESIAN_POINT('Ctrl Pts',(100.76032631584,10.1485536062597,48.0816078414171));
#110058=CARTESIAN_POINT('Ctrl Pts',(100.788174905153,9.85408835187024,48.1070402666074));
#110059=CARTESIAN_POINT('Ctrl Pts',(101.182828978934,9.38785877941283,48.1535247162687));
#110060=CARTESIAN_POINT('Ctrl Pts',(102.006402006358,9.49026281080507,48.2166807896812));
#110061=CARTESIAN_POINT('Ctrl Pts',(102.371142746215,10.2357255210765,48.279836863094));
#110062=CARTESIAN_POINT('Ctrl Pts',(101.946587511935,10.9488247522485,48.3429929365066));
#110063=CARTESIAN_POINT('Ctrl Pts',(101.117382546223,10.9834348473594,48.4061490099193));
#110064=CARTESIAN_POINT('Ctrl Pts',(100.775542341,10.5050687063655,48.4508938446496));
#110065=CARTESIAN_POINT('Ctrl Pts',(100.759991095274,10.2310561302136,48.474586654909));
#110066=CARTESIAN_POINT('Ctrl Pts',(100.76022353047,10.200488094229,48.4772274406976));
#110067=CARTESIAN_POINT('Ctrl Pts',(100.760222148438,10.2004868904783,48.1562725593024));
#110068=CARTESIAN_POINT('Ctrl Pts',(100.761849372691,9.98739349496877,48.1746821771012));
#110069=CARTESIAN_POINT('Ctrl Pts',(100.970123675266,9.5278414290224,48.2141438193708));
#110070=CARTESIAN_POINT('Ctrl Pts',(101.74831434399,9.3642331418485,48.2746574861114));
#110071=CARTESIAN_POINT('Ctrl Pts',(102.335460969162,9.95071284574935,48.337813559524));
#110072=CARTESIAN_POINT('Ctrl Pts',(102.165712572132,10.7631006363966,48.4009696329368));
#110073=CARTESIAN_POINT('Ctrl Pts',(101.392626626404,11.065204620822,48.4641257063493));
#110074=CARTESIAN_POINT('Ctrl Pts',(100.838969225623,10.6704097524001,48.5158933484713));
#110075=CARTESIAN_POINT('Ctrl Pts',(100.76186233198,10.3127360326821,48.5466089661223));
#110076=CARTESIAN_POINT('Ctrl Pts',(100.762038832931,10.2001239241621,48.5562725593024));
#110077=CARTESIAN_POINT('Origin',(101.5,10.2,45.0772274406976));
#110078=CARTESIAN_POINT('',(100.762115591849,10.2001619360863,47.6772274406976));
#110079=CARTESIAN_POINT('',(100.760786028196,10.1993577218161,47.7562725593024));
#110080=CARTESIAN_POINT('',(100.761,10.2,45.0772274406976));
#110081=CARTESIAN_POINT('Ctrl Pts',(100.762115591849,10.2001619360863,47.6772274406976));
#110082=CARTESIAN_POINT('Ctrl Pts',(100.762378749843,10.0673212625574,47.6886290279251));
#110083=CARTESIAN_POINT('Ctrl Pts',(100.859902638249,9.68884167169019,47.7210826396234));
#110084=CARTESIAN_POINT('Ctrl Pts',(101.463865885969,9.32887186093604,47.7745882757927));
#110085=CARTESIAN_POINT('Ctrl Pts',(102.209501304701,9.69326751848885,47.8377443492053));
#110086=CARTESIAN_POINT('Ctrl Pts',(102.312288916283,10.5167910365686,47.900900422618));
#110087=CARTESIAN_POINT('Ctrl Pts',(101.679097556161,11.0532842761012,47.9640564960306));
#110088=CARTESIAN_POINT('Ctrl Pts',(100.9388056778,10.8330664826122,48.0228321687239));
#110089=CARTESIAN_POINT('Ctrl Pts',(100.762538637766,10.3927160141838,48.0605558169462));
#110090=CARTESIAN_POINT('Ctrl Pts',(100.760786644801,10.199357707728,48.0772274406976));
#110091=CARTESIAN_POINT('Ctrl Pts',(100.760786028196,10.1993577218161,47.7562725593024));
#110092=CARTESIAN_POINT('Ctrl Pts',(100.760325879463,10.1485725191587,47.7606513391383));
#110093=CARTESIAN_POINT('Ctrl Pts',(100.788162216564,9.8541264402612,47.7860821434451));
#110094=CARTESIAN_POINT('Ctrl Pts',(101.182767392066,9.3878833576509,47.8325649722227));
#110095=CARTESIAN_POINT('Ctrl Pts',(102.006346869156,9.49022344047391,47.8957210456354));
#110096=CARTESIAN_POINT('Ctrl Pts',(102.371147367118,10.2356604419514,47.958877119048));
#110097=CARTESIAN_POINT('Ctrl Pts',(101.946640733675,10.9487875878849,48.0220331924607));
#110098=CARTESIAN_POINT('Ctrl Pts',(101.117450646044,10.9834703820361,48.0851892658734));
#110099=CARTESIAN_POINT('Ctrl Pts',(100.775543514179,10.5050992334164,48.1299357214873));
#110100=CARTESIAN_POINT('Ctrl Pts',(100.759988586379,10.2310730447501,48.1536301526303));
#110101=CARTESIAN_POINT('Ctrl Pts',(100.760222148438,10.2004868904783,48.1562725593024));
#110102=CARTESIAN_POINT('Origin',(101.5,10.2,45.0772274406976));
#110103=CARTESIAN_POINT('',(100.760218090122,10.2004849659209,47.2772274406976));
#110104=CARTESIAN_POINT('',(100.762115726615,10.2001616419592,47.3562725593024));
#110105=CARTESIAN_POINT('',(100.761,10.2,45.0772274406976));
#110106=CARTESIAN_POINT('Ctrl Pts',(100.760218090122,10.2004849659209,47.2772274406976));
#110107=CARTESIAN_POINT('Ctrl Pts',(100.761842905485,9.98724259353902,47.2956502144331));
#110108=CARTESIAN_POINT('Ctrl Pts',(100.970375642338,9.52755072013085,47.3351250126394));
#110109=CARTESIAN_POINT('Ctrl Pts',(101.748822022916,9.36438196436754,47.3956518353166));
#110110=CARTESIAN_POINT('Ctrl Pts',(102.335637038891,9.95124180430941,47.4588079087293));
#110111=CARTESIAN_POINT('Ctrl Pts',(102.165318282924,10.7634904454937,47.521963982142));
#110112=CARTESIAN_POINT('Ctrl Pts',(101.392184050584,11.0651853109369,47.5851200555546));
#110113=CARTESIAN_POINT('Ctrl Pts',(100.838675749468,10.670027787286,47.6368745417399));
#110114=CARTESIAN_POINT('Ctrl Pts',(100.761892851834,10.3125998412386,47.6675770034542));
#110115=CARTESIAN_POINT('Ctrl Pts',(100.762115591849,10.2001619360863,47.6772274406976));
#110116=CARTESIAN_POINT('Ctrl Pts',(100.762115726615,10.2001616419592,47.3562725593024));
#110117=CARTESIAN_POINT('Ctrl Pts',(100.762378367007,10.0673397991113,47.3676725256463));
#110118=CARTESIAN_POINT('Ctrl Pts',(100.859881900044,9.68887966549334,47.400124516461));
#110119=CARTESIAN_POINT('Ctrl Pts',(101.463799353238,9.32887464035278,47.4536285317467));
#110120=CARTESIAN_POINT('Ctrl Pts',(102.209462575557,9.69321332531287,47.5167846051594));
#110121=CARTESIAN_POINT('Ctrl Pts',(102.31231312286,10.5167290045424,47.579940678572));
#110122=CARTESIAN_POINT('Ctrl Pts',(101.679162679895,11.0532705437534,47.6430967519847));
#110123=CARTESIAN_POINT('Ctrl Pts',(100.93883371831,10.8331033354341,47.7018740455615));
#110124=CARTESIAN_POINT('Ctrl Pts',(100.76253815383,10.3927344476349,47.7395993146674));
#110125=CARTESIAN_POINT('Ctrl Pts',(100.760786028196,10.1993577218161,47.7562725593024));
#110126=CARTESIAN_POINT('Origin',(101.5,10.2,45.0772274406976));
#110127=CARTESIAN_POINT('',(100.760790554215,10.1993571884951,46.8772274406976));
#110128=CARTESIAN_POINT('',(100.760218566757,10.2004851870816,46.9562725593024));
#110129=CARTESIAN_POINT('',(100.761,10.2,45.0772274406976));
#110130=CARTESIAN_POINT('Ctrl Pts',(100.760790554216,10.1993571884951,46.8772274406976));
#110131=CARTESIAN_POINT('Ctrl Pts',(100.760328944673,10.1484185953511,46.8816193764702));
#110132=CARTESIAN_POINT('Ctrl Pts',(100.78826499662,9.8538170750545,46.9070633367136));
#110133=CARTESIAN_POINT('Ctrl Pts',(101.18327099084,9.38768686529745,46.953559321428));
#110134=CARTESIAN_POINT('Ctrl Pts',(102.006786682075,9.49053741410128,47.0167153948406));
#110135=CARTESIAN_POINT('Ctrl Pts',(102.371125372346,10.2362006472893,47.0798714682533));
#110136=CARTESIAN_POINT('Ctrl Pts',(101.946175880112,10.9490640718669,47.143027541666));
#110137=CARTESIAN_POINT('Ctrl Pts',(101.116966152284,10.983233663854,47.2061836150786));
#110138=CARTESIAN_POINT('Ctrl Pts',(100.775453563156,10.5047900625241,47.2509169147559));
#110139=CARTESIAN_POINT('Ctrl Pts',(100.759986200666,10.2309183671265,47.2745981899622));
#110140=CARTESIAN_POINT('Ctrl Pts',(100.760218090122,10.2004849659209,47.2772274406976));
#110141=CARTESIAN_POINT('Ctrl Pts',(100.760218566757,10.2004851870817,46.9562725593024));
#110142=CARTESIAN_POINT('Ctrl Pts',(100.761843790147,9.98726122745261,46.9746937121543));
#110143=CARTESIAN_POINT('Ctrl Pts',(100.970345134679,9.52758681490828,47.0141668894771));
#110144=CARTESIAN_POINT('Ctrl Pts',(101.748758192064,9.36436297329056,47.0746920912707));
#110145=CARTESIAN_POINT('Ctrl Pts',(102.335618023451,9.95117798071123,47.1378481646834));
#110146=CARTESIAN_POINT('Ctrl Pts',(102.165361312267,10.7634396172603,47.201004238096));
#110147=CARTESIAN_POINT('Ctrl Pts',(101.392250136753,11.065193530587,47.2641603115087));
#110148=CARTESIAN_POINT('Ctrl Pts',(100.838694327669,10.6700659187596,47.3159164185775));
#110149=CARTESIAN_POINT('Ctrl Pts',(100.761893355754,10.312618478149,47.3466205011754));
#110150=CARTESIAN_POINT('Ctrl Pts',(100.762115726615,10.2001616419592,47.3562725593024));
#110151=CARTESIAN_POINT('Origin',(101.5,10.2,45.0772274406976));
#110152=CARTESIAN_POINT('',(100.762114836837,10.2001642984427,46.4772274406976));
#110153=CARTESIAN_POINT('',(100.760790004998,10.1993572533204,46.5562725593024));
#110154=CARTESIAN_POINT('',(100.761,10.2,45.0772274406976));
#110155=CARTESIAN_POINT('Ctrl Pts',(100.762114836837,10.2001642984427,46.4772274406976));
#110156=CARTESIAN_POINT('Ctrl Pts',(100.762381617085,10.0671895096557,46.4886405629782));
#110157=CARTESIAN_POINT('Ctrl Pts',(100.860050119229,9.688570906901,46.5211057097297));
#110158=CARTESIAN_POINT('Ctrl Pts',(101.464339557519,9.32885262012148,46.574622880952));
#110159=CARTESIAN_POINT('Ctrl Pts',(102.209776569879,9.69365312349436,46.6377789543647));
#110160=CARTESIAN_POINT('Ctrl Pts',(102.312116654185,10.5172326125426,46.7009350277773));
#110161=CARTESIAN_POINT('Ctrl Pts',(101.678633633533,11.0533814325012,46.76409110119));
#110162=CARTESIAN_POINT('Ctrl Pts',(100.938607013354,10.8328047227516,46.8228552388301));
#110163=CARTESIAN_POINT('Ctrl Pts',(100.762541594375,10.3925843948781,46.8605673519993));
#110164=CARTESIAN_POINT('Ctrl Pts',(100.760790554216,10.1993571884951,46.8772274406976));
#110165=CARTESIAN_POINT('Ctrl Pts',(100.760790004998,10.1993572533204,46.5562725593024));
#110166=CARTESIAN_POINT('Ctrl Pts',(100.760328571292,10.1484375546355,46.5606628741914));
#110167=CARTESIAN_POINT('Ctrl Pts',(100.788252312888,9.8538551645519,46.5861052135513));
#110168=CARTESIAN_POINT('Ctrl Pts',(101.183208968053,9.38771109556577,46.6325995773821));
#110169=CARTESIAN_POINT('Ctrl Pts',(102.006732474123,9.49049870563814,46.6957556507947));
#110170=CARTESIAN_POINT('Ctrl Pts',(102.371128126366,10.2361341135068,46.7589117242074));
#110171=CARTESIAN_POINT('Ctrl Pts',(101.946233085569,10.9490299761907,46.82206779762));
#110172=CARTESIAN_POINT('Ctrl Pts',(101.11702598516,10.9832629084246,46.8852238710328));
#110173=CARTESIAN_POINT('Ctrl Pts',(100.775464480548,10.5048280645237,46.9299587915935));
#110174=CARTESIAN_POINT('Ctrl Pts',(100.759986455655,10.2309373997303,46.9536416876834));
#110175=CARTESIAN_POINT('Ctrl Pts',(100.760218566757,10.2004851870817,46.9562725593024));
#110176=CARTESIAN_POINT('Origin',(101.5,10.2,45.0772274406976));
#110177=CARTESIAN_POINT('',(100.760229243717,10.2005121657882,46.0772274406976));
#110178=CARTESIAN_POINT('',(100.762116465727,10.2001659521564,46.1562725593024));
#110179=CARTESIAN_POINT('',(100.761,10.2,45.0772274406976));
#110180=CARTESIAN_POINT('Ctrl Pts',(100.760229243717,10.2005121657882,46.0772274406976));
#110181=CARTESIAN_POINT('Ctrl Pts',(100.761855102872,9.98714653281361,46.0956617494862));
#110182=CARTESIAN_POINT('Ctrl Pts',(100.970571497003,9.52725163041578,46.1351480827457));
#110183=CARTESIAN_POINT('Ctrl Pts',(101.749287158062,9.36453901572865,46.195686440476));
#110184=CARTESIAN_POINT('Ctrl Pts',(102.335766870331,9.95168565395949,46.2588425138887));
#110185=CARTESIAN_POINT('Ctrl Pts',(102.165014415475,10.7638570231953,46.3219985873013));
#110186=CARTESIAN_POINT('Ctrl Pts',(101.39171255474,11.0651241681623,46.385154660714));
#110187=CARTESIAN_POINT('Ctrl Pts',(100.838543929659,10.669756891461,46.4368976118461));
#110188=CARTESIAN_POINT('Ctrl Pts',(100.761889528753,10.3124675710606,46.4675885385073));
#110189=CARTESIAN_POINT('Ctrl Pts',(100.762114836837,10.2001642984427,46.4772274406976));
#110190=CARTESIAN_POINT('Ctrl Pts',(100.762116465727,10.2001659521564,46.1562725593024));
#110191=CARTESIAN_POINT('Ctrl Pts',(100.762382064326,10.0672091272765,46.1676840606994));
#110192=CARTESIAN_POINT('Ctrl Pts',(100.860027014519,9.68860582926417,46.2001475865673));
#110193=CARTESIAN_POINT('Ctrl Pts',(101.464274479552,9.32885726690886,46.2536631369061));
#110194=CARTESIAN_POINT('Ctrl Pts',(102.209737178785,9.69359800080378,46.3168192103187));
#110195=CARTESIAN_POINT('Ctrl Pts',(102.312141208784,10.5171710165563,46.3799752837314));
#110196=CARTESIAN_POINT('Ctrl Pts',(101.678698651257,11.0533675611342,46.4431313571441));
#110197=CARTESIAN_POINT('Ctrl Pts',(100.938635007123,10.8328415897021,46.5018971156678));
#110198=CARTESIAN_POINT('Ctrl Pts',(100.762541194739,10.3926028980946,46.5396108497205));
#110199=CARTESIAN_POINT('Ctrl Pts',(100.760790004998,10.1993572533204,46.5562725593024));
#110200=CARTESIAN_POINT('Origin',(101.5,10.2,48.71675));
#110201=CARTESIAN_POINT('Ctrl Pts',(102.101843294079,10.6308187385845,48.71675));
#110202=CARTESIAN_POINT('Ctrl Pts',(102.092690583018,10.6489925625313,48.71675));
#110203=CARTESIAN_POINT('Ctrl Pts',(102.082761232596,10.6667230538167,48.71675));
#110204=CARTESIAN_POINT('Ctrl Pts',(102.072068380608,10.6839544004916,48.71675));
#110205=CARTESIAN_POINT('Ctrl Pts',(102.054494347484,10.7122746519614,48.71675));
#110206=CARTESIAN_POINT('Ctrl Pts',(102.034860699482,10.7392477510368,48.71675));
#110207=CARTESIAN_POINT('Ctrl Pts',(102.01341340141,10.7648111233467,48.71675));
#110208=CARTESIAN_POINT('Ctrl Pts',(102.006324556343,10.7732604294126,48.71675));
#110209=CARTESIAN_POINT('Ctrl Pts',(101.999037195898,10.7815556229965,48.71675));
#110210=CARTESIAN_POINT('Ctrl Pts',(101.991559132777,10.7896940729177,48.71675));
#110211=CARTESIAN_POINT('Ctrl Pts',(101.985554234903,10.7962292625578,48.71675));
#110212=CARTESIAN_POINT('Ctrl Pts',(101.979427179349,10.8026622683498,48.71675));
#110213=CARTESIAN_POINT('Ctrl Pts',(101.973191056542,10.8089830617106,48.71675));
#110214=CARTESIAN_POINT('Ctrl Pts',(101.948142429081,10.8343717852865,48.71675));
#110215=CARTESIAN_POINT('Ctrl Pts',(101.921302301576,10.8579911576652,48.71675));
#110216=CARTESIAN_POINT('Ctrl Pts',(101.89295359764,10.8797678614235,48.71675));
#110217=CARTESIAN_POINT('Ctrl Pts',(101.872371173306,10.8955787203034,48.71675));
#110218=CARTESIAN_POINT('Ctrl Pts',(101.850992282563,10.9104180010441,48.71675));
#110219=CARTESIAN_POINT('Ctrl Pts',(101.828910233771,10.9242499170876,48.71675));
#110220=CARTESIAN_POINT('Ctrl Pts',(101.821834677165,10.9286819562456,48.71675));
#110221=CARTESIAN_POINT('Ctrl Pts',(101.814689271962,10.9330088612385,48.71675));
#110222=CARTESIAN_POINT('Ctrl Pts',(101.807486420978,10.9372243553017,48.71675));
#110223=CARTESIAN_POINT('Ctrl Pts',(101.774891643114,10.9563005645511,48.71675));
#110224=CARTESIAN_POINT('Ctrl Pts',(101.741072447943,10.973130235416,48.71675));
#110225=CARTESIAN_POINT('Ctrl Pts',(101.706330263218,10.9876331586578,48.71675));
#110226=CARTESIAN_POINT('Ctrl Pts',(101.671325142582,11.0022458429686,48.71675));
#110227=CARTESIAN_POINT('Ctrl Pts',(101.635381961669,11.0144973135584,48.71675));
#110228=CARTESIAN_POINT('Ctrl Pts',(101.598767749634,11.0242717697334,48.71675));
#110229=CARTESIAN_POINT('Ctrl Pts',(101.579580093906,11.029394067595,48.71675));
#110230=CARTESIAN_POINT('Ctrl Pts',(101.560207566501,11.0338354689131,48.71675));
#110231=CARTESIAN_POINT('Ctrl Pts',(101.540685650761,11.0375743770417,48.71675));
#110232=CARTESIAN_POINT('Ctrl Pts',(101.53155005331,11.0393240598099,48.71675));
#110233=CARTESIAN_POINT('Ctrl Pts',(101.522380019735,11.040919918186,48.71675));
#110234=CARTESIAN_POINT('Ctrl Pts',(101.513201010965,11.0423565975106,48.71675));
#110235=CARTESIAN_POINT('Ctrl Pts',(101.473716936833,11.0485365625134,48.71675));
#110236=CARTESIAN_POINT('Ctrl Pts',(101.43398096282,11.0517930196521,48.71675));
#110237=CARTESIAN_POINT('Ctrl Pts',(101.394302526066,11.0520184237927,48.71675));
#110238=CARTESIAN_POINT('Ctrl Pts',(101.356654041365,11.052232296239,48.71675));
#110239=CARTESIAN_POINT('Ctrl Pts',(101.319055963889,11.0497182152357,48.71675));
#110240=CARTESIAN_POINT('Ctrl Pts',(101.281703678425,11.0446512493134,48.71675));
#110241=CARTESIAN_POINT('Ctrl Pts',(101.26460477746,11.0423317246196,48.71675));
#110242=CARTESIAN_POINT('Ctrl Pts',(101.24755721676,11.0394765171797,48.71675));
#110243=CARTESIAN_POINT('Ctrl Pts',(101.23057927414,11.0360989397513,48.71675));
#110244=CARTESIAN_POINT('Ctrl Pts',(101.221478845773,11.0342885082916,48.71675));
#110245=CARTESIAN_POINT('Ctrl Pts',(101.212398417896,11.0323279573613,48.71675));
#110246=CARTESIAN_POINT('Ctrl Pts',(101.203340811571,11.0302190898984,48.71675));
#110247=CARTESIAN_POINT('Ctrl Pts',(101.195132556756,11.0283079755393,48.71675));
#110248=CARTESIAN_POINT('Ctrl Pts',(101.186950940351,11.0262768354341,48.71675));
#110249=CARTESIAN_POINT('Ctrl Pts',(101.178803613277,11.024129252906,48.71675));
#110250=CARTESIAN_POINT('Ctrl Pts',(101.140506034481,11.0140342597457,48.71675));
#110251=CARTESIAN_POINT('Ctrl Pts',(101.102928410637,11.0013616719051,48.71675));
#110252=CARTESIAN_POINT('Ctrl Pts',(101.066285661362,10.9863186497589,48.71675));
#110253=CARTESIAN_POINT('Ctrl Pts',(101.028791532849,10.9709261091683,48.71675));
#110254=CARTESIAN_POINT('Ctrl Pts',(100.992275134187,10.9530515299956,48.71675));
#110255=CARTESIAN_POINT('Ctrl Pts',(100.956964088485,10.9328624060656,48.71675));
#110256=CARTESIAN_POINT('Ctrl Pts',(100.940025732422,10.9231778848934,48.71675));
#110257=CARTESIAN_POINT('Ctrl Pts',(100.923364796535,10.9129600041663,48.71675));
#110258=CARTESIAN_POINT('Ctrl Pts',(100.907007375654,10.9022231657751,48.71675));
#110259=CARTESIAN_POINT('Ctrl Pts',(100.900112212376,10.8976972533868,48.71675));
#110260=CARTESIAN_POINT('Ctrl Pts',(100.893270992315,10.8930790974484,48.71675));
#110261=CARTESIAN_POINT('Ctrl Pts',(100.88648573145,10.8883696454142,48.71675));
#110262=CARTESIAN_POINT('Ctrl Pts',(100.87935004954,10.8834169763343,48.71675));
#110263=CARTESIAN_POINT('Ctrl Pts',(100.872282874817,10.8783678650625,48.71675));
#110264=CARTESIAN_POINT('Ctrl Pts',(100.865291068121,10.8732276252648,48.71675));
#110265=CARTESIAN_POINT('Ctrl Pts',(100.831195079059,10.8481609196874,48.71675));
#110266=CARTESIAN_POINT('Ctrl Pts',(100.798854446776,10.8209060995123,48.71675));
#110267=CARTESIAN_POINT('Ctrl Pts',(100.768506288754,10.791658862854,48.71675));
#110268=CARTESIAN_POINT('Ctrl Pts',(100.738364625154,10.7626106297466,48.71675));
#110269=CARTESIAN_POINT('Ctrl Pts',(100.710187233691,10.7315964626783,48.71675));
#110270=CARTESIAN_POINT('Ctrl Pts',(100.684223172419,10.6987607209512,48.71675));
#110271=CARTESIAN_POINT('Ctrl Pts',(100.665548276792,10.6751433044338,48.71675));
#110272=CARTESIAN_POINT('Ctrl Pts',(100.648018699993,10.6505825193258,48.71675));
#110273=CARTESIAN_POINT('Ctrl Pts',(100.631737776319,10.625119128515,48.71675));
#110274=CARTESIAN_POINT('',(100.630604630375,9.77384666716111,48.71675));
#110275=CARTESIAN_POINT('Origin',(101.5,10.2,48.71675));
#110276=CARTESIAN_POINT('Ctrl Pts',(100.630581430873,9.77382549334316,48.71675));
#110277=CARTESIAN_POINT('Ctrl Pts',(100.64457938054,9.75169648824875,48.71675));
#110278=CARTESIAN_POINT('Ctrl Pts',(100.659509975824,9.73021546929278,48.71675));
#110279=CARTESIAN_POINT('Ctrl Pts',(100.675375864845,9.70945200083441,48.71675));
#110280=CARTESIAN_POINT('Ctrl Pts',(100.698139903374,9.6796610199839,48.71675));
#110281=CARTESIAN_POINT('Ctrl Pts',(100.722828987013,9.65134590823789,48.71675));
#110282=CARTESIAN_POINT('Ctrl Pts',(100.749246101771,9.62460368156239,48.71675));
#110283=CARTESIAN_POINT('Ctrl Pts',(100.759494608228,9.61422904810002,48.71675));
#110284=CARTESIAN_POINT('Ctrl Pts',(100.770003353453,9.60409144395543,48.71675));
#110285=CARTESIAN_POINT('Ctrl Pts',(100.780761309316,9.59419773022566,48.71675));
#110286=CARTESIAN_POINT('Ctrl Pts',(100.791070498368,9.58471673155325,48.71675));
#110287=CARTESIAN_POINT('Ctrl Pts',(100.801612891683,9.57545635783652,48.71675));
#110288=CARTESIAN_POINT('Ctrl Pts',(100.812354121759,9.56644314416643,48.71675));
#110289=CARTESIAN_POINT('Ctrl Pts',(100.844321982801,9.53961817532173,48.71675));
#110290=CARTESIAN_POINT('Ctrl Pts',(100.878082193053,9.51494593631547,48.71675));
#110291=CARTESIAN_POINT('Ctrl Pts',(100.913359655757,9.49256416154415,48.71675));
#110292=CARTESIAN_POINT('Ctrl Pts',(100.93382034179,9.47958288592574,48.71675));
#110293=CARTESIAN_POINT('Ctrl Pts',(100.954791816909,9.4673729974237,48.71675));
#110294=CARTESIAN_POINT('Ctrl Pts',(100.976221881509,9.45596930559344,48.71675));
#110295=CARTESIAN_POINT('Ctrl Pts',(100.984317998785,9.45166107656292,48.71675));
#110296=CARTESIAN_POINT('Ctrl Pts',(100.992479570662,9.44746797593293,48.71675));
#110297=CARTESIAN_POINT('Ctrl Pts',(101.000703773174,9.44339211164565,48.71675));
#110298=CARTESIAN_POINT('Ctrl Pts',(101.00844277817,9.43955670827007,48.71675));
#110299=CARTESIAN_POINT('Ctrl Pts',(101.016232654013,9.43582746843061,48.71675));
#110300=CARTESIAN_POINT('Ctrl Pts',(101.024063874372,9.43220886794855,48.71675));
#110301=CARTESIAN_POINT('Ctrl Pts',(101.060487154985,9.41537863016349,48.71675));
#110302=CARTESIAN_POINT('Ctrl Pts',(101.097850508457,9.40091469113947,48.71675));
#110303=CARTESIAN_POINT('Ctrl Pts',(101.135908601312,9.38894508905378,48.71675));
#110304=CARTESIAN_POINT('Ctrl Pts',(101.173086380745,9.37725235321574,48.71675));
#110305=CARTESIAN_POINT('Ctrl Pts',(101.210928218599,9.36793981658584,48.71675));
#110306=CARTESIAN_POINT('Ctrl Pts',(101.249203335133,9.36117504344504,48.71675));
#110307=CARTESIAN_POINT('Ctrl Pts',(101.26756945998,9.35792900060259,48.71675));
#110308=CARTESIAN_POINT('Ctrl Pts',(101.286035216727,9.3552703122121,48.71675));
#110309=CARTESIAN_POINT('Ctrl Pts',(101.304573852963,9.35322165048947,48.71675));
#110310=CARTESIAN_POINT('Ctrl Pts',(101.312743136943,9.35231888185126,48.71675));
#110311=CARTESIAN_POINT('Ctrl Pts',(101.320926558308,9.35153460646509,48.71675));
#110312=CARTESIAN_POINT('Ctrl Pts',(101.32912174998,9.35087093707399,48.71675));
#110313=CARTESIAN_POINT('Ctrl Pts',(101.337079548327,9.35022649245393,48.71675));
#110314=CARTESIAN_POINT('Ctrl Pts',(101.345042813093,9.34969629700434,48.71675));
#110315=CARTESIAN_POINT('Ctrl Pts',(101.353001912458,9.34928206049807,48.71675));
#110316=CARTESIAN_POINT('Ctrl Pts',(101.39019525861,9.34734630859198,48.71675));
#110317=CARTESIAN_POINT('Ctrl Pts',(101.427349750722,9.34793465249878,48.71675));
#110318=CARTESIAN_POINT('Ctrl Pts',(101.464257143167,9.35118601291411,48.71675));
#110319=CARTESIAN_POINT('Ctrl Pts',(101.497915149683,9.35415111835223,48.71675));
#110320=CARTESIAN_POINT('Ctrl Pts',(101.53136812566,9.35933215400883,48.71675));
#110321=CARTESIAN_POINT('Ctrl Pts',(101.564442234567,9.36663343101134,48.71675));
#110322=CARTESIAN_POINT('Ctrl Pts',(101.581998310551,9.37050902367491,48.71675));
#110323=CARTESIAN_POINT('Ctrl Pts',(101.599447362032,9.37498247030888,48.71675));
#110324=CARTESIAN_POINT('Ctrl Pts',(101.61676102719,9.38004213013849,48.71675));
#110325=CARTESIAN_POINT('Ctrl Pts',(101.627764250115,9.38325765755686,48.71675));
#110326=CARTESIAN_POINT('Ctrl Pts',(101.638712756026,9.38670998442451,48.71675));
#110327=CARTESIAN_POINT('Ctrl Pts',(101.649598833322,9.39039643608377,48.71675));
#110328=CARTESIAN_POINT('Ctrl Pts',(101.657334704852,9.39301610482793,48.71675));
#110329=CARTESIAN_POINT('Ctrl Pts',(101.665031702681,9.39575158311581,48.71675));
#110330=CARTESIAN_POINT('Ctrl Pts',(101.672681658731,9.39859908201335,48.71675));
#110331=CARTESIAN_POINT('Ctrl Pts',(101.707638773391,9.4116109666317,48.71675));
#110332=CARTESIAN_POINT('Ctrl Pts',(101.741655218118,9.42697182351799,48.71675));
#110333=CARTESIAN_POINT('Ctrl Pts',(101.774500046676,9.44453787650665,48.71675));
#110334=CARTESIAN_POINT('Ctrl Pts',(101.806936769189,9.46188566644687,48.71675));
#110335=CARTESIAN_POINT('Ctrl Pts',(101.838231681605,9.48138516613843,48.71675));
#110336=CARTESIAN_POINT('Ctrl Pts',(101.86812362857,9.50292993629208,48.71675));
#110337=CARTESIAN_POINT('Ctrl Pts',(101.882249726167,9.51311139172793,48.71675));
#110338=CARTESIAN_POINT('Ctrl Pts',(101.896061863265,9.52374998245355,48.71675));
#110339=CARTESIAN_POINT('Ctrl Pts',(101.909528589229,9.53483608185471,48.71675));
#110340=CARTESIAN_POINT('Ctrl Pts',(101.916887297398,9.54089392920632,48.71675));
#110341=CARTESIAN_POINT('Ctrl Pts',(101.924145165926,9.54708773163212,48.71675));
#110342=CARTESIAN_POINT('Ctrl Pts',(101.931278238249,9.55339893605095,48.71675));
#110343=CARTESIAN_POINT('Ctrl Pts',(101.957731009864,9.57680383670771,48.71675));
#110344=CARTESIAN_POINT('Ctrl Pts',(101.982525561837,9.60186412427372,48.71675));
#110345=CARTESIAN_POINT('Ctrl Pts',(102.005439886383,9.62847142275743,48.71675));
#110346=CARTESIAN_POINT('Ctrl Pts',(102.027519731796,9.65410975375978,48.71675));
#110347=CARTESIAN_POINT('Ctrl Pts',(102.047854190426,9.68118532379663,48.71675));
#110348=CARTESIAN_POINT('Ctrl Pts',(102.066199893377,9.70961703269809,48.71675));
#110349=CARTESIAN_POINT('Ctrl Pts',(102.078805695628,9.72915318789655,48.71675));
#110350=CARTESIAN_POINT('Ctrl Pts',(102.090471602248,9.74932995292834,48.71675));
#110351=CARTESIAN_POINT('Ctrl Pts',(102.101104350279,9.77012262204778,48.71675));
#110352=CARTESIAN_POINT('Ctrl Pts',(101.175031770393,10.8637142832168,45.6852584761921));
#110353=CARTESIAN_POINT('Ctrl Pts',(100.955551792886,10.756252350382,45.706310500663));
#110354=CARTESIAN_POINT('Ctrl Pts',(100.635341557809,10.3080724084119,45.7484145496047));
#110355=CARTESIAN_POINT('Ctrl Pts',(100.936604150766,9.53400264453299,45.8115706230174));
#110356=CARTESIAN_POINT('Ctrl Pts',(101.749341902197,9.36467411870078,45.8747266964301));
#110357=CARTESIAN_POINT('Ctrl Pts',(102.33569099053,9.95154749830959,45.9378827698427));
#110358=CARTESIAN_POINT('Ctrl Pts',(102.165084835389,10.7638419256677,46.0010388432554));
#110359=CARTESIAN_POINT('Ctrl Pts',(101.391765482636,11.0651152556269,46.0641949166681));
#110360=CARTESIAN_POINT('Ctrl Pts',(100.716565164316,10.5826174497482,46.1273509900807));
#110361=CARTESIAN_POINT('Ctrl Pts',(100.751175258495,9.75341249376129,46.1905070634934));
#110362=CARTESIAN_POINT('Ctrl Pts',(101.464274479552,9.32885726690886,46.2536631369061));
#110363=CARTESIAN_POINT('Ctrl Pts',(102.209737178785,9.69359800080378,46.3168192103187));
#110364=CARTESIAN_POINT('Ctrl Pts',(102.312141208784,10.5171710165563,46.3799752837314));
#110365=CARTESIAN_POINT('Ctrl Pts',(101.678698651257,11.0533675611342,46.4431313571441));
#110366=CARTESIAN_POINT('Ctrl Pts',(100.883345795901,10.8163663755618,46.5062874305568));
#110367=CARTESIAN_POINT('Ctrl Pts',(100.646715736332,10.020902446434,46.5694435039694));
#110368=CARTESIAN_POINT('Ctrl Pts',(101.183208968053,9.38771109556577,46.6325995773821));
#110369=CARTESIAN_POINT('Ctrl Pts',(102.006732474123,9.49049870563814,46.6957556507947));
#110370=CARTESIAN_POINT('Ctrl Pts',(102.371128126366,10.2361341135068,46.7589117242074));
#110371=CARTESIAN_POINT('Ctrl Pts',(101.946233085569,10.9490299761907,46.82206779762));
#110372=CARTESIAN_POINT('Ctrl Pts',(101.11702598516,10.9832629084246,46.8852238710328));
#110373=CARTESIAN_POINT('Ctrl Pts',(100.634814701675,10.3078159478443,46.9483799444453));
#110374=CARTESIAN_POINT('Ctrl Pts',(100.936509562721,9.53468172677525,47.0115360178581));
#110375=CARTESIAN_POINT('Ctrl Pts',(101.748758192064,9.36436297329056,47.0746920912707));
#110376=CARTESIAN_POINT('Ctrl Pts',(102.335618023451,9.95117798071123,47.1378481646834));
#110377=CARTESIAN_POINT('Ctrl Pts',(102.165361312267,10.7634396172603,47.201004238096));
#110378=CARTESIAN_POINT('Ctrl Pts',(101.392250136753,11.065193530587,47.2641603115087));
#110379=CARTESIAN_POINT('Ctrl Pts',(100.716766347564,10.5830338421318,47.3273163849214));
#110380=CARTESIAN_POINT('Ctrl Pts',(100.750935939053,9.75382412639255,47.390472458334));
#110381=CARTESIAN_POINT('Ctrl Pts',(101.463799353238,9.32887464035278,47.4536285317467));
#110382=CARTESIAN_POINT('Ctrl Pts',(102.209462575557,9.69321332531287,47.5167846051594));
#110383=CARTESIAN_POINT('Ctrl Pts',(102.31231312286,10.5167290045424,47.579940678572));
#110384=CARTESIAN_POINT('Ctrl Pts',(101.679162679895,11.0532705437534,47.6430967519847));
#110385=CARTESIAN_POINT('Ctrl Pts',(100.883680829641,10.8167013598813,47.7062528253974));
#110386=CARTESIAN_POINT('Ctrl Pts',(100.646618579947,10.0213663690729,47.7694088988101));
#110387=CARTESIAN_POINT('Ctrl Pts',(101.182767392066,9.3878833576509,47.8325649722227));
#110388=CARTESIAN_POINT('Ctrl Pts',(102.006346869156,9.49022344047391,47.8957210456354));
#110389=CARTESIAN_POINT('Ctrl Pts',(102.371147367118,10.2356604419514,47.958877119048));
#110390=CARTESIAN_POINT('Ctrl Pts',(101.946640733675,10.9487875878849,48.0220331924607));
#110391=CARTESIAN_POINT('Ctrl Pts',(101.117450646044,10.9834703820361,48.0851892658734));
#110392=CARTESIAN_POINT('Ctrl Pts',(100.634875844886,10.3082874437177,48.148345339286));
#110393=CARTESIAN_POINT('Ctrl Pts',(100.936142984193,9.53498559418258,48.2115014126987));
#110394=CARTESIAN_POINT('Ctrl Pts',(101.74831434399,9.3642331418485,48.2746574861114));
#110395=CARTESIAN_POINT('Ctrl Pts',(102.335460969162,9.95071284574935,48.337813559524));
#110396=CARTESIAN_POINT('Ctrl Pts',(102.165712572132,10.7631006363966,48.4009696329368));
#110397=CARTESIAN_POINT('Ctrl Pts',(101.392626626404,11.065204620822,48.4641257063493));
#110398=CARTESIAN_POINT('Ctrl Pts',(100.717169409966,10.5835583129935,48.527281779762));
#110399=CARTESIAN_POINT('Ctrl Pts',(100.750281720561,9.75402930376689,48.5904378531747));
#110400=CARTESIAN_POINT('Ctrl Pts',(101.464139111132,9.32935204372765,48.6535939265874));
#110401=CARTESIAN_POINT('Ctrl Pts',(101.958950595826,9.57134677434548,48.6956979755291));
#110402=CARTESIAN_POINT('Ctrl Pts',(102.101104350279,9.77012262204778,48.71675));
#110403=CARTESIAN_POINT('Ctrl Pts',(101.141648137424,10.931896930038,45.7290889841281));
#110404=CARTESIAN_POINT('Ctrl Pts',(100.899621220414,10.81339554966,45.7501410085989));
#110405=CARTESIAN_POINT('Ctrl Pts',(100.546516135974,10.3191745694474,45.7922450575407));
#110406=CARTESIAN_POINT('Ctrl Pts',(100.878727107616,9.46558546018134,45.8554011309534));
#110407=CARTESIAN_POINT('Ctrl Pts',(101.774956524761,9.27886199895974,45.9185572043661));
#110408=CARTESIAN_POINT('Ctrl Pts',(102.421540617545,9.92602424289236,45.9817132777787));
#110409=CARTESIAN_POINT('Ctrl Pts',(102.233408277545,10.8217647937645,46.0448693511913));
#110410=CARTESIAN_POINT('Ctrl Pts',(101.380646668324,11.15398760541,46.1080254246041));
#110411=CARTESIAN_POINT('Ctrl Pts',(100.636083755282,10.6219233244348,46.1711814980167));
#110412=CARTESIAN_POINT('Ctrl Pts',(100.674249306813,9.70753504471038,46.2343375714294));
#110413=CARTESIAN_POINT('Ctrl Pts',(101.460604435672,9.23936572091811,46.297493644842));
#110414=CARTESIAN_POINT('Ctrl Pts',(102.282647707639,9.64157587391296,46.3606497182547));
#110415=CARTESIAN_POINT('Ctrl Pts',(102.395571592321,10.5497536503049,46.4238057916674));
#110416=CARTESIAN_POINT('Ctrl Pts',(101.697056169445,11.1410330830324,46.48696186508));
#110417=CARTESIAN_POINT('Ctrl Pts',(100.819997579851,10.8796850232994,46.5501179384927));
#110418=CARTESIAN_POINT('Ctrl Pts',(100.559058771492,10.0025039494449,46.6132740119053));
#110419=CARTESIAN_POINT('Ctrl Pts',(101.15066536971,9.30426553941562,46.6764300853181));
#110420=CARTESIAN_POINT('Ctrl Pts',(102.058788550343,9.41761240893498,46.7395861587307));
#110421=CARTESIAN_POINT('Ctrl Pts',(102.460618171823,10.2398461317076,46.8027422321434));
#110422=CARTESIAN_POINT('Ctrl Pts',(101.992074125369,11.0259770114083,46.865898305556));
#110423=CARTESIAN_POINT('Ctrl Pts',(101.077683480929,11.0637266555575,46.9290543789687));
#110424=CARTESIAN_POINT('Ctrl Pts',(100.545935156482,10.3188917629645,46.9922104523813));
#110425=CARTESIAN_POINT('Ctrl Pts',(100.878622802644,9.46633430380414,47.055366525794));
#110426=CARTESIAN_POINT('Ctrl Pts',(101.774312850721,9.27851888991975,47.1185225992067));
#110427=CARTESIAN_POINT('Ctrl Pts',(102.421460154638,9.9256167651528,47.1816786726194));
#110428=CARTESIAN_POINT('Ctrl Pts',(102.233713156592,10.8213211566518,47.244834746032));
#110429=CARTESIAN_POINT('Ctrl Pts',(101.381181110432,11.1540739214716,47.3079908194447));
#110430=CARTESIAN_POINT('Ctrl Pts',(100.636305605867,10.6223824923553,47.3711468928573));
#110431=CARTESIAN_POINT('Ctrl Pts',(100.673985402345,9.70798896391439,47.43430296627));
#110432=CARTESIAN_POINT('Ctrl Pts',(101.460080500149,9.23938487911703,47.4974590396827));
#110433=CARTESIAN_POINT('Ctrl Pts',(102.282344894719,9.64115168112703,47.5606151130954));
#110434=CARTESIAN_POINT('Ctrl Pts',(102.395761166942,10.5492662308773,47.623771186508));
#110435=CARTESIAN_POINT('Ctrl Pts',(101.697567867241,11.1409260991615,47.6869272599207));
#110436=CARTESIAN_POINT('Ctrl Pts',(100.820367031243,10.8800544201938,47.7500833333334));
#110437=CARTESIAN_POINT('Ctrl Pts',(100.558951634338,10.0030155303523,47.813239406746));
#110438=CARTESIAN_POINT('Ctrl Pts',(101.150178431102,9.30445549779749,47.8763954801587));
#110439=CARTESIAN_POINT('Ctrl Pts',(102.058363332597,9.41730886607965,47.9395515535713));
#110440=CARTESIAN_POINT('Ctrl Pts',(102.460639389158,10.2393238003883,48.002707626984));
#110441=CARTESIAN_POINT('Ctrl Pts',(101.992523650723,11.0257097228153,48.0658637003966));
#110442=CARTESIAN_POINT('Ctrl Pts',(101.078151766765,11.0639554427076,48.1290197738094));
#110443=CARTESIAN_POINT('Ctrl Pts',(100.546002580868,10.3194116950965,48.192175847222));
#110444=CARTESIAN_POINT('Ctrl Pts',(100.878218565903,9.46666938717991,48.2553319206347));
#110445=CARTESIAN_POINT('Ctrl Pts',(101.773823406617,9.27837572103478,48.3184879940473));
#110446=CARTESIAN_POINT('Ctrl Pts',(102.421286966332,9.92510384738192,48.38164406746));
#110447=CARTESIAN_POINT('Ctrl Pts',(102.234100501002,10.8209473526525,48.4448001408727));
#110448=CARTESIAN_POINT('Ctrl Pts',(101.381596276455,11.1540861509944,48.5079562142854));
#110449=CARTESIAN_POINT('Ctrl Pts',(100.636750074431,10.6229608415385,48.571112287698));
#110450=CARTESIAN_POINT('Ctrl Pts',(100.673263976699,9.70821521893735,48.6342683611107));
#110451=CARTESIAN_POINT('Ctrl Pts',(101.460455161001,9.23991132562163,48.6974244345233));
#110452=CARTESIAN_POINT('Ctrl Pts',(102.006098091631,9.50676591185436,48.7395284834651));
#110453=CARTESIAN_POINT('Ctrl Pts',(102.16285514675,9.72596178631092,48.760580507936));
#110454=CARTESIAN_POINT('Ctrl Pts',(101.108264504454,11.0000795768592,45.772919492064));
#110455=CARTESIAN_POINT('Ctrl Pts',(100.843690647942,10.8705387489381,45.7939715165349));
#110456=CARTESIAN_POINT('Ctrl Pts',(100.457690714139,10.330276730483,45.8360755654767));
#110457=CARTESIAN_POINT('Ctrl Pts',(100.820850064466,9.39716827582969,45.8992316388894));
#110458=CARTESIAN_POINT('Ctrl Pts',(101.800571147326,9.1930498792187,45.962387712302));
#110459=CARTESIAN_POINT('Ctrl Pts',(102.507390244561,9.90050098747513,46.0255437857147));
#110460=CARTESIAN_POINT('Ctrl Pts',(102.301731719701,10.8796876618614,46.0886998591274));
#110461=CARTESIAN_POINT('Ctrl Pts',(101.369527854013,11.242859955193,46.15185593254));
#110462=CARTESIAN_POINT('Ctrl Pts',(100.555602346249,10.6612291991214,46.2150120059527));
#110463=CARTESIAN_POINT('Ctrl Pts',(100.597323355132,9.66165759565947,46.2781680793654));
#110464=CARTESIAN_POINT('Ctrl Pts',(101.456934391792,9.14987417492735,46.341324152778));
#110465=CARTESIAN_POINT('Ctrl Pts',(102.355558236492,9.58955374702215,46.4044802261907));
#110466=CARTESIAN_POINT('Ctrl Pts',(102.479001975857,10.5823362840535,46.4676362996034));
#110467=CARTESIAN_POINT('Ctrl Pts',(101.715413687634,11.2286986049306,46.530792373016));
#110468=CARTESIAN_POINT('Ctrl Pts',(100.7566493638,10.943003671037,46.5939484464287));
#110469=CARTESIAN_POINT('Ctrl Pts',(100.471401806652,9.98410545245592,46.6571045198413));
#110470=CARTESIAN_POINT('Ctrl Pts',(101.118121771367,9.22081998326547,46.7202605932541));
#110471=CARTESIAN_POINT('Ctrl Pts',(102.110844626564,9.34472611223181,46.7834166666666));
#110472=CARTESIAN_POINT('Ctrl Pts',(102.550108217281,10.2435581499084,46.8465727400794));
#110473=CARTESIAN_POINT('Ctrl Pts',(102.03791516517,11.1029240466259,46.909728813492));
#110474=CARTESIAN_POINT('Ctrl Pts',(101.038340976698,11.1441904026905,46.9728848869047));
#110475=CARTESIAN_POINT('Ctrl Pts',(100.457055611289,10.3299675780847,47.0360409603173));
#110476=CARTESIAN_POINT('Ctrl Pts',(100.820736042567,9.39798688083304,47.09919703373));
#110477=CARTESIAN_POINT('Ctrl Pts',(101.799867509378,9.19267480654896,47.1623531071427));
#110478=CARTESIAN_POINT('Ctrl Pts',(102.507302285824,9.90005554959437,47.2255091805554));
#110479=CARTESIAN_POINT('Ctrl Pts',(102.302065000918,10.8792026960433,47.288665253968));
#110480=CARTESIAN_POINT('Ctrl Pts',(101.370112084111,11.2429543123562,47.3518213273806));
#110481=CARTESIAN_POINT('Ctrl Pts',(100.55584486417,10.6617311425788,47.4149774007933));
#110482=CARTESIAN_POINT('Ctrl Pts',(100.597034865638,9.66215380143623,47.478133474206));
#110483=CARTESIAN_POINT('Ctrl Pts',(101.456361647059,9.14989511788128,47.5412895476187));
#110484=CARTESIAN_POINT('Ctrl Pts',(102.355227213882,9.5890900369412,47.6044456210314));
#110485=CARTESIAN_POINT('Ctrl Pts',(102.479209211025,10.5818034572122,47.667601694444));
#110486=CARTESIAN_POINT('Ctrl Pts',(101.715973054587,11.2285816545697,47.7307577678567));
#110487=CARTESIAN_POINT('Ctrl Pts',(100.757053232844,10.9434074805064,47.7939138412693));
#110488=CARTESIAN_POINT('Ctrl Pts',(100.471284688728,9.98466469163163,47.857069914682));
#110489=CARTESIAN_POINT('Ctrl Pts',(101.117589470138,9.22102763794408,47.9202259880947));
#110490=CARTESIAN_POINT('Ctrl Pts',(102.110379796039,9.3443942916854,47.9833820615074));
#110491=CARTESIAN_POINT('Ctrl Pts',(102.550131411197,10.2429871588251,48.04653813492));
#110492=CARTESIAN_POINT('Ctrl Pts',(102.038406567771,11.1026318577458,48.1096942083327));
#110493=CARTESIAN_POINT('Ctrl Pts',(101.038852887485,11.1444405033791,48.1728502817453));
#110494=CARTESIAN_POINT('Ctrl Pts',(100.457129316851,10.3305359464753,48.236006355158));
#110495=CARTESIAN_POINT('Ctrl Pts',(100.820294147612,9.39835318017724,48.2991624285707));
#110496=CARTESIAN_POINT('Ctrl Pts',(101.799332469244,9.19251830022108,48.3623185019833));
#110497=CARTESIAN_POINT('Ctrl Pts',(102.507112963503,9.89949484901449,48.425474575396));
#110498=CARTESIAN_POINT('Ctrl Pts',(102.302488429871,10.8787940689084,48.4886306488086));
#110499=CARTESIAN_POINT('Ctrl Pts',(101.370565926506,11.2429676811668,48.5517867222213));
#110500=CARTESIAN_POINT('Ctrl Pts',(100.556330738897,10.6623633700836,48.614942795634));
#110501=CARTESIAN_POINT('Ctrl Pts',(100.596246232837,9.66240113410781,48.6780988690466));
#110502=CARTESIAN_POINT('Ctrl Pts',(101.45677121087,9.15047060751563,48.7412549424594));
#110503=CARTESIAN_POINT('Ctrl Pts',(102.053245587436,9.44218504936324,48.7833589914011));
#110504=CARTESIAN_POINT('Ctrl Pts',(102.224605943221,9.68180095057406,48.804411015872));
#110505=CARTESIAN_POINT('Ctrl Pts',(101.074880871485,11.0682622236804,45.81675));
#110506=CARTESIAN_POINT('Ctrl Pts',(100.78776007547,10.9276819482162,45.8378020244709));
#110507=CARTESIAN_POINT('Ctrl Pts',(100.368865292303,10.3413788915185,45.8799060734127));
#110508=CARTESIAN_POINT('Ctrl Pts',(100.762973021317,9.32875109147804,45.9430621468253));
#110509=CARTESIAN_POINT('Ctrl Pts',(101.82618576989,9.10723775947766,46.006218220238));
#110510=CARTESIAN_POINT('Ctrl Pts',(102.593239871576,9.8749777320579,46.0693742936507));
#110511=CARTESIAN_POINT('Ctrl Pts',(102.370055161857,10.9376105299583,46.1325303670633));
#110512=CARTESIAN_POINT('Ctrl Pts',(101.358409039701,11.3317323049761,46.195686440476));
#110513=CARTESIAN_POINT('Ctrl Pts',(100.475120937215,10.7005350738079,46.2588425138886));
#110514=CARTESIAN_POINT('Ctrl Pts',(100.52039740345,9.61578014660857,46.3219985873014));
#110515=CARTESIAN_POINT('Ctrl Pts',(101.453264347912,9.0603826289366,46.385154660714));
#110516=CARTESIAN_POINT('Ctrl Pts',(102.428468765346,9.53753162013133,46.4483107341267));
#110517=CARTESIAN_POINT('Ctrl Pts',(102.562432359394,10.6149189178021,46.5114668075393));
#110518=CARTESIAN_POINT('Ctrl Pts',(101.733771205822,11.3163641268288,46.574622880952));
#110519=CARTESIAN_POINT('Ctrl Pts',(100.69330114775,11.0063223187746,46.6377789543647));
#110520=CARTESIAN_POINT('Ctrl Pts',(100.383744841812,9.96570695546689,46.7009350277773));
#110521=CARTESIAN_POINT('Ctrl Pts',(101.085578173025,9.13737442711531,46.76409110119));
#110522=CARTESIAN_POINT('Ctrl Pts',(102.162900702785,9.27183981552865,46.8272471746026));
#110523=CARTESIAN_POINT('Ctrl Pts',(102.639598262739,10.2472701681092,46.8904032480154));
#110524=CARTESIAN_POINT('Ctrl Pts',(102.083756204971,11.1798710818435,46.953559321428));
#110525=CARTESIAN_POINT('Ctrl Pts',(100.998998472468,11.2246541498234,47.0167153948407));
#110526=CARTESIAN_POINT('Ctrl Pts',(100.368176066096,10.341043393205,47.0798714682533));
#110527=CARTESIAN_POINT('Ctrl Pts',(100.762849282491,9.32963945786195,47.1430275416661));
#110528=CARTESIAN_POINT('Ctrl Pts',(101.825422168035,9.10683072317815,47.2061836150786));
#110529=CARTESIAN_POINT('Ctrl Pts',(102.593144417011,9.87449433403596,47.2693396884914));
#110530=CARTESIAN_POINT('Ctrl Pts',(102.370416845243,10.9370842354348,47.3324957619039));
#110531=CARTESIAN_POINT('Ctrl Pts',(101.359043057789,11.3318347032408,47.3956518353167));
#110532=CARTESIAN_POINT('Ctrl Pts',(100.475384122473,10.7010797928023,47.4588079087293));
#110533=CARTESIAN_POINT('Ctrl Pts',(100.52008432893,9.61631863895806,47.521963982142));
#110534=CARTESIAN_POINT('Ctrl Pts',(101.452642793969,9.06040535664555,47.5851200555546));
#110535=CARTESIAN_POINT('Ctrl Pts',(102.428109533044,9.53702839275536,47.6482761289673));
#110536=CARTESIAN_POINT('Ctrl Pts',(102.562657255108,10.6143406835471,47.71143220238));
#110537=CARTESIAN_POINT('Ctrl Pts',(101.734378241932,11.3162372099778,47.7745882757927));
#110538=CARTESIAN_POINT('Ctrl Pts',(100.693739434446,11.006760540819,47.8377443492053));
#110539=CARTESIAN_POINT('Ctrl Pts',(100.383617743118,9.96631385291099,47.900900422618));
#110540=CARTESIAN_POINT('Ctrl Pts',(101.085000509175,9.13759977809068,47.9640564960307));
#110541=CARTESIAN_POINT('Ctrl Pts',(102.162396259481,9.27147971729114,48.0272125694433));
#110542=CARTESIAN_POINT('Ctrl Pts',(102.639623433236,10.2466505172619,48.090368642856));
#110543=CARTESIAN_POINT('Ctrl Pts',(102.084289484818,11.1795539926762,48.1535247162686));
#110544=CARTESIAN_POINT('Ctrl Pts',(100.999554008205,11.2249255640506,48.2166807896813));
#110545=CARTESIAN_POINT('Ctrl Pts',(100.368256052833,10.341660197854,48.2798368630939));
#110546=CARTESIAN_POINT('Ctrl Pts',(100.762369729322,9.33003697317457,48.3429929365066));
#110547=CARTESIAN_POINT('Ctrl Pts',(101.824841531871,9.10666087940736,48.4061490099193));
#110548=CARTESIAN_POINT('Ctrl Pts',(102.592938960673,9.87388585064706,48.469305083332));
#110549=CARTESIAN_POINT('Ctrl Pts',(102.37087635874,10.9366407851643,48.5324611567447));
#110550=CARTESIAN_POINT('Ctrl Pts',(101.359535576557,11.3318492113392,48.5956172301573));
#110551=CARTESIAN_POINT('Ctrl Pts',(100.475911403362,10.7017658986286,48.65877330357));
#110552=CARTESIAN_POINT('Ctrl Pts',(100.519228488975,9.61658704927828,48.7219293769826));
#110553=CARTESIAN_POINT('Ctrl Pts',(101.45308726074,9.06102988940963,48.7850854503953));
#110554=CARTESIAN_POINT('Ctrl Pts',(102.100393083241,9.37760418687212,48.8271894993371));
#110555=CARTESIAN_POINT('Ctrl Pts',(102.286356739692,9.6376401148372,48.848241523808));
#110556=CARTESIAN_POINT('Ctrl Pts',(100.534608987464,10.2001621159456,48.6877640831103));
#110557=CARTESIAN_POINT('Ctrl Pts',(100.53483984494,10.052869158678,48.6974260554069));
#110558=CARTESIAN_POINT('Ctrl Pts',(100.56702615616,9.90546817974631,48.7070880277034));
#110559=CARTESIAN_POINT('Ctrl Pts',(100.630581430873,9.77382549334327,48.71675));
#110560=CARTESIAN_POINT('',(101.070122622048,9.59889564972058,45.81675));
#110561=CARTESIAN_POINT('Ctrl Pts',(101.06918126624,9.59815671460027,45.81675));
#110562=CARTESIAN_POINT('Ctrl Pts',(101.05100744208,9.60730942634728,45.81675));
#110563=CARTESIAN_POINT('Ctrl Pts',(101.033276950503,9.61723877762716,45.81675));
#110564=CARTESIAN_POINT('Ctrl Pts',(101.016045603448,9.62793163066911,45.81675));
#110565=CARTESIAN_POINT('Ctrl Pts',(100.987725351354,9.64550566552492,45.81675));
#110566=CARTESIAN_POINT('Ctrl Pts',(100.960752251418,9.66513931578662,45.81675));
#110567=CARTESIAN_POINT('Ctrl Pts',(100.935188878082,9.6865866164717,45.81675));
#110568=CARTESIAN_POINT('Ctrl Pts',(100.92673957253,9.69367546168651,45.81675));
#110569=CARTESIAN_POINT('Ctrl Pts',(100.918444379411,9.70096282227849,45.81675));
#110570=CARTESIAN_POINT('Ctrl Pts',(100.910305929908,9.70844088554085,45.81675));
#110571=CARTESIAN_POINT('Ctrl Pts',(100.90377074013,9.71444578396391,45.81675));
#110572=CARTESIAN_POINT('Ctrl Pts',(100.897337734181,9.72057284008257,45.81675));
#110573=CARTESIAN_POINT('Ctrl Pts',(100.891016940649,9.72680896346648,45.81675));
#110574=CARTESIAN_POINT('Ctrl Pts',(100.865628216618,9.75185759301389,45.81675));
#110575=CARTESIAN_POINT('Ctrl Pts',(100.842008843511,9.77869772275828,45.81675));
#110576=CARTESIAN_POINT('Ctrl Pts',(100.820232138824,9.80704642891589,45.81675));
#110577=CARTESIAN_POINT('Ctrl Pts',(100.804421280313,9.82762885350541,45.81675));
#110578=CARTESIAN_POINT('Ctrl Pts',(100.789581999707,9.84900774438982,45.81675));
#110579=CARTESIAN_POINT('Ctrl Pts',(100.775750083582,9.87108979316409,45.81675));
#110580=CARTESIAN_POINT('Ctrl Pts',(100.771318045365,9.87816534821914,45.81675));
#110581=CARTESIAN_POINT('Ctrl Pts',(100.766991141235,9.88531075184123,45.81675));
#110582=CARTESIAN_POINT('Ctrl Pts',(100.762775647967,9.8925136012006,45.81675));
#110583=CARTESIAN_POINT('Ctrl Pts',(100.743699436389,9.92510838183202,45.81675));
#110584=CARTESIAN_POINT('Ctrl Pts',(100.726869763159,9.95892757967534,45.81675));
#110585=CARTESIAN_POINT('Ctrl Pts',(100.712366837593,9.99366976676314,45.81675));
#110586=CARTESIAN_POINT('Ctrl Pts',(100.69775415064,10.0286748904987,45.81675));
#110587=CARTESIAN_POINT('Ctrl Pts',(100.685502677547,10.0646180742379,45.81675));
#110588=CARTESIAN_POINT('Ctrl Pts',(100.675728219088,10.1012322885948,45.81675));
#110589=CARTESIAN_POINT('Ctrl Pts',(100.670605920794,10.1204199426764,45.81675));
#110590=CARTESIAN_POINT('Ctrl Pts',(100.6661645189,10.1397924682425,45.81675));
#110591=CARTESIAN_POINT('Ctrl Pts',(100.662425610055,10.1593143819321,45.81675));
#110592=CARTESIAN_POINT('Ctrl Pts',(100.660675925445,10.1684499862913,45.81675));
#110593=CARTESIAN_POINT('Ctrl Pts',(100.659080065457,10.1776200268081,45.81675));
#110594=CARTESIAN_POINT('Ctrl Pts',(100.657643384766,10.186799042495,45.81675));
#110595=CARTESIAN_POINT('Ctrl Pts',(100.651463417681,10.2262831221287,45.81675));
#110596=CARTESIAN_POINT('Ctrl Pts',(100.648206959382,10.2660191009013,45.81675));
#110597=CARTESIAN_POINT('Ctrl Pts',(100.647981555128,10.3056975413403,45.81675));
#110598=CARTESIAN_POINT('Ctrl Pts',(100.647767682598,10.3433460255231,45.81675));
#110599=CARTESIAN_POINT('Ctrl Pts',(100.650281763879,10.3809441015259,45.81675));
#110600=CARTESIAN_POINT('Ctrl Pts',(100.655348730347,10.4182963848193,45.81675));
#110601=CARTESIAN_POINT('Ctrl Pts',(100.657668255377,10.4353952854263,45.81675));
#110602=CARTESIAN_POINT('Ctrl Pts',(100.660523463249,10.4524428456175,45.81675));
#110603=CARTESIAN_POINT('Ctrl Pts',(100.663901041196,10.4694207875995,45.81675));
#110604=CARTESIAN_POINT('Ctrl Pts',(100.665711473481,10.4785212183748,45.81675));
#110605=CARTESIAN_POINT('Ctrl Pts',(100.667672025352,10.4876016486112,45.81675));
#110606=CARTESIAN_POINT('Ctrl Pts',(100.669780893868,10.4966592572468,45.81675));
#110607=CARTESIAN_POINT('Ctrl Pts',(100.671692007865,10.5048675085044,45.81675));
#110608=CARTESIAN_POINT('Ctrl Pts',(100.67372314753,10.5130491213257,45.81675));
#110609=CARTESIAN_POINT('Ctrl Pts',(100.675870729547,10.5211964448257,45.81675));
#110610=CARTESIAN_POINT('Ctrl Pts',(100.685965723623,10.559494019415,45.81675));
#110611=CARTESIAN_POINT('Ctrl Pts',(100.698638312468,10.5970716385837,45.81675));
#110612=CARTESIAN_POINT('Ctrl Pts',(100.713681335617,10.6337143830086,45.81675));
#110613=CARTESIAN_POINT('Ctrl Pts',(100.729073877235,10.6712085065637,45.81675));
#110614=CARTESIAN_POINT('Ctrl Pts',(100.746948457436,10.707724900083,45.81675));
#110615=CARTESIAN_POINT('Ctrl Pts',(100.7671375823,10.7430359407574,45.81675));
#110616=CARTESIAN_POINT('Ctrl Pts',(100.776822104117,10.7599742947513,45.81675));
#110617=CARTESIAN_POINT('Ctrl Pts',(100.787039985488,10.7766352285847,45.81675));
#110618=CARTESIAN_POINT('Ctrl Pts',(100.797776824513,10.7929926474574,45.81675));
#110619=CARTESIAN_POINT('Ctrl Pts',(100.8023027384,10.7998878117669,45.81675));
#110620=CARTESIAN_POINT('Ctrl Pts',(100.806920895886,10.8067290328366,45.81675));
#110621=CARTESIAN_POINT('Ctrl Pts',(100.811630349515,10.8135142946914,45.81675));
#110622=CARTESIAN_POINT('Ctrl Pts',(100.816583018343,10.8206499748645,45.81675));
#110623=CARTESIAN_POINT('Ctrl Pts',(100.821632129333,10.8277171478722,45.81675));
#110624=CARTESIAN_POINT('Ctrl Pts',(100.826772368825,10.8347089528894,45.81675));
#110625=CARTESIAN_POINT('Ctrl Pts',(100.851839075462,10.8688049372315,45.81675));
#110626=CARTESIAN_POINT('Ctrl Pts',(100.879093896518,10.9011455652106,45.81675));
#110627=CARTESIAN_POINT('Ctrl Pts',(100.908341133779,10.9314937196515,45.81675));
#110628=CARTESIAN_POINT('Ctrl Pts',(100.937389369515,10.9616353818016,45.81675));
#110629=CARTESIAN_POINT('Ctrl Pts',(100.968403539212,10.9898127722535,45.81675));
#110630=CARTESIAN_POINT('Ctrl Pts',(101.001239283439,11.0157768332061,45.81675));
#110631=CARTESIAN_POINT('Ctrl Pts',(101.024856698805,11.0344517262696,45.81675));
#110632=CARTESIAN_POINT('Ctrl Pts',(101.04941748246,11.051981301149,45.81675));
#110633=CARTESIAN_POINT('Ctrl Pts',(101.074880871485,11.0682622236804,45.81675));
#110634=CARTESIAN_POINT('Ctrl Pts',(101.06918126624,9.59815671460025,45.81675));
#110635=CARTESIAN_POINT('Ctrl Pts',(101.251697602369,9.46914978142767,45.8360755654767));
#110636=CARTESIAN_POINT('Ctrl Pts',(101.765370568999,9.38071711773372,45.8764531554243));
#110637=CARTESIAN_POINT('Ctrl Pts',(102.33569099053,9.95154749830959,45.9378827698427));
#110638=CARTESIAN_POINT('Ctrl Pts',(102.165084835389,10.7638419256677,46.0010388432554));
#110639=CARTESIAN_POINT('Ctrl Pts',(101.391765482636,11.0651152556269,46.0641949166681));
#110640=CARTESIAN_POINT('Ctrl Pts',(100.838565297627,10.669798683291,46.1159394886837));
#110641=CARTESIAN_POINT('Ctrl Pts',(100.761892086014,10.3124888878941,46.1466320362285));
#110642=CARTESIAN_POINT('Ctrl Pts',(100.762116465727,10.2001659521564,46.1562725593024));
#110643=CARTESIAN_POINT('Origin',(101.5,10.2,45.81675));
#110644=CARTESIAN_POINT('',(100.53325,10.2,45.81675));
#110645=CARTESIAN_POINT('Origin',(101.5,10.2,45.81675));
#110646=CARTESIAN_POINT('Origin',(101.5,10.2,45.81675));
#110647=CARTESIAN_POINT('',(101.929877377952,9.59889564972063,45.81675));
#110648=CARTESIAN_POINT('Ctrl Pts',(101.926174511012,11.0694185813664,45.81675));
#110649=CARTESIAN_POINT('Ctrl Pts',(101.948303515656,11.0554206324422,45.81675));
#110650=CARTESIAN_POINT('Ctrl Pts',(101.969784534031,11.0404900380945,45.81675));
#110651=CARTESIAN_POINT('Ctrl Pts',(101.990548001762,11.0246241502298,45.81675));
#110652=CARTESIAN_POINT('Ctrl Pts',(102.020338981568,11.001860113359,45.81675));
#110653=CARTESIAN_POINT('Ctrl Pts',(102.048654091966,10.977171031833,45.81675));
#110654=CARTESIAN_POINT('Ctrl Pts',(102.075396317082,10.9507539194945,45.81675));
#110655=CARTESIAN_POINT('Ctrl Pts',(102.085770950475,10.940505413447,45.81675));
#110656=CARTESIAN_POINT('Ctrl Pts',(102.095908554493,10.9299966686515,45.81675));
#110657=CARTESIAN_POINT('Ctrl Pts',(102.105802268045,10.919238713229,45.81675));
#110658=CARTESIAN_POINT('Ctrl Pts',(102.11528326565,10.9089295255755,45.81675));
#110659=CARTESIAN_POINT('Ctrl Pts',(102.124543638292,10.8983871337153,45.81675));
#110660=CARTESIAN_POINT('Ctrl Pts',(102.13355685089,10.8876459051365,45.81675));
#110661=CARTESIAN_POINT('Ctrl Pts',(102.16038181785,10.8556780469933,45.81675));
#110662=CARTESIAN_POINT('Ctrl Pts',(102.185054054778,10.8219178398454,45.81675));
#110663=CARTESIAN_POINT('Ctrl Pts',(102.207435827403,10.7866403802508,45.81675));
#110664=CARTESIAN_POINT('Ctrl Pts',(102.220417101675,10.7661796961809,45.81675));
#110665=CARTESIAN_POINT('Ctrl Pts',(102.232626988819,10.7452082230353,45.81675));
#110666=CARTESIAN_POINT('Ctrl Pts',(102.244030679305,10.723778160377,45.81675));
#110667=CARTESIAN_POINT('Ctrl Pts',(102.248338908853,10.7156820419094,45.81675));
#110668=CARTESIAN_POINT('Ctrl Pts',(102.252532009947,10.7075204688054,45.81675));
#110669=CARTESIAN_POINT('Ctrl Pts',(102.256607874645,10.699296265029,45.81675));
#110670=CARTESIAN_POINT('Ctrl Pts',(102.260443278273,10.6915572591171,45.81675));
#110671=CARTESIAN_POINT('Ctrl Pts',(102.26417251832,10.6837673823401,45.81675));
#110672=CARTESIAN_POINT('Ctrl Pts',(102.267791118971,10.6759361610197,45.81675));
#110673=CARTESIAN_POINT('Ctrl Pts',(102.284621354702,10.6395128820778,45.81675));
#110674=CARTESIAN_POINT('Ctrl Pts',(102.299085291605,10.6021495300482,45.81675));
#110675=CARTESIAN_POINT('Ctrl Pts',(102.311054891601,10.56409143824,45.81675));
#110676=CARTESIAN_POINT('Ctrl Pts',(102.322747625754,10.5269136586982,45.81675));
#110677=CARTESIAN_POINT('Ctrl Pts',(102.332060160583,10.4890718203185,45.81675));
#110678=CARTESIAN_POINT('Ctrl Pts',(102.338824931882,10.4507967026999,45.81675));
#110679=CARTESIAN_POINT('Ctrl Pts',(102.342070973874,10.4324305771433,45.81675));
#110680=CARTESIAN_POINT('Ctrl Pts',(102.344729661393,10.4139648195556,45.81675));
#110681=CARTESIAN_POINT('Ctrl Pts',(102.346778322229,10.3954261823324,45.81675));
#110682=CARTESIAN_POINT('Ctrl Pts',(102.347681092635,10.3872568783932,45.81675));
#110683=CARTESIAN_POINT('Ctrl Pts',(102.348465369219,10.3790734369715,45.81675));
#110684=CARTESIAN_POINT('Ctrl Pts',(102.349129039225,10.3708782251626,45.81675));
#110685=CARTESIAN_POINT('Ctrl Pts',(102.349773484486,10.3629204067042,45.81675));
#110686=CARTESIAN_POINT('Ctrl Pts',(102.35030368,10.354957121918,45.81675));
#110687=CARTESIAN_POINT('Ctrl Pts',(102.350717915998,10.3469980024824,45.81675));
#110688=CARTESIAN_POINT('Ctrl Pts',(102.35265365805,10.3098047063077,45.81675));
#110689=CARTESIAN_POINT('Ctrl Pts',(102.352065311248,10.2726502636654,45.81675));
#110690=CARTESIAN_POINT('Ctrl Pts',(102.348813955523,10.2357429191864,45.81675));
#110691=CARTESIAN_POINT('Ctrl Pts',(102.345848851563,10.2020849246283,45.81675));
#110692=CARTESIAN_POINT('Ctrl Pts',(102.34066781952,10.1686319597464,45.81675));
#110693=CARTESIAN_POINT('Ctrl Pts',(102.333366548057,10.1355578610452,45.81675));
#110694=CARTESIAN_POINT('Ctrl Pts',(102.32949095817,10.1180017897395,45.81675));
#110695=CARTESIAN_POINT('Ctrl Pts',(102.325017514806,10.1005527426951,45.81675));
#110696=CARTESIAN_POINT('Ctrl Pts',(102.319957858714,10.0832390817281,45.81675));
#110697=CARTESIAN_POINT('Ctrl Pts',(102.3167422658,10.0722356292209,45.81675));
#110698=CARTESIAN_POINT('Ctrl Pts',(102.313289863631,10.0612868959364,45.81675));
#110699=CARTESIAN_POINT('Ctrl Pts',(102.309603327023,10.0504005939673,45.81675));
#110700=CARTESIAN_POINT('Ctrl Pts',(102.306983713134,10.0426649030276,45.81675));
#110701=CARTESIAN_POINT('Ctrl Pts',(102.30424829546,10.0349680849826,45.81675));
#110702=CARTESIAN_POINT('Ctrl Pts',(102.301400862263,10.027318306124,45.81675));
#110703=CARTESIAN_POINT('Ctrl Pts',(102.288388975775,9.99236118955888,45.81675));
#110704=CARTESIAN_POINT('Ctrl Pts',(102.2730281174,9.95834474272888,45.81675));
#110705=CARTESIAN_POINT('Ctrl Pts',(102.255462063125,9.92549991214507,45.81675));
#110706=CARTESIAN_POINT('Ctrl Pts',(102.238114273384,9.89306319037982,45.81675));
#110707=CARTESIAN_POINT('Ctrl Pts',(102.218614774453,9.86176827859395,45.81675));
#110708=CARTESIAN_POINT('Ctrl Pts',(102.197070005432,9.83187633235799,45.81675));
#110709=CARTESIAN_POINT('Ctrl Pts',(102.18688854255,9.81775022402949,45.81675));
#110710=CARTESIAN_POINT('Ctrl Pts',(102.176249943744,9.80393807671464,45.81675));
#110711=CARTESIAN_POINT('Ctrl Pts',(102.165163835632,9.79047134114548,45.81675));
#110712=CARTESIAN_POINT('Ctrl Pts',(102.159106008442,9.78311265800195,45.81675));
#110713=CARTESIAN_POINT('Ctrl Pts',(102.15291222714,9.77585481388914,45.81675));
#110714=CARTESIAN_POINT('Ctrl Pts',(102.146601044657,9.76872176517651,45.81675));
#110715=CARTESIAN_POINT('Ctrl Pts',(102.123196147213,9.74226899281033,45.81675));
#110716=CARTESIAN_POINT('Ctrl Pts',(102.09813586298,9.71747444018442,45.81675));
#110717=CARTESIAN_POINT('Ctrl Pts',(102.071528567788,9.69456011526773,45.81675));
#110718=CARTESIAN_POINT('Ctrl Pts',(102.04589024096,9.67248027035965,45.81675));
#110719=CARTESIAN_POINT('Ctrl Pts',(102.018814675174,9.65214581235937,45.81675));
#110720=CARTESIAN_POINT('Ctrl Pts',(101.990382970443,9.63380011029726,45.81675));
#110721=CARTESIAN_POINT('Ctrl Pts',(101.970846814486,9.62119430631815,45.81675));
#110722=CARTESIAN_POINT('Ctrl Pts',(101.95067004842,9.60952839844149,45.81675));
#110723=CARTESIAN_POINT('Ctrl Pts',(101.929877377952,9.59889564972062,45.81675));
#110724=CARTESIAN_POINT('Origin',(101.5,10.2,45.81675));
#110725=CARTESIAN_POINT('Origin',(101.5,10.2,45.0772274406976));
#110726=CARTESIAN_POINT('Ctrl Pts',(101.929877377952,9.59889564972062,45.81675));
#110727=CARTESIAN_POINT('Ctrl Pts',(102.128653225655,9.74104940417406,45.8378020244709));
#110728=CARTESIAN_POINT('Ctrl Pts',(102.370647903658,10.23586098604,45.8799060734127));
#110729=CARTESIAN_POINT('Ctrl Pts',(101.945970715424,10.9497182652191,45.9430621468254));
#110730=CARTESIAN_POINT('Ctrl Pts',(101.116441674876,10.9828306195272,46.006218220238));
#110731=CARTESIAN_POINT('Ctrl Pts',(100.775380687848,10.5045291878666,46.0509399848621));
#110732=CARTESIAN_POINT('Ctrl Pts',(100.759998367851,10.2308105930258,46.0746097250153));
#110733=CARTESIAN_POINT('Ctrl Pts',(100.760229243717,10.2005121657882,46.0772274406976));
#110734=CARTESIAN_POINT('Ctrl Pts',(102.062359885163,9.41364326030773,45.6852584761921));
#110735=CARTESIAN_POINT('Ctrl Pts',(102.322395813128,9.5996069167595,45.706310500663));
#110736=CARTESIAN_POINT('Ctrl Pts',(102.638970041762,10.2469128663792,45.7484145496048));
#110737=CARTESIAN_POINT('Ctrl Pts',(102.083412975827,11.1807714924229,45.8115706230174));
#110738=CARTESIAN_POINT('Ctrl Pts',(100.998234085503,11.2240886352204,45.8747266964301));
#110739=CARTESIAN_POINT('Ctrl Pts',(100.36815077501,10.3404644127608,45.9378827698427));
#110740=CARTESIAN_POINT('Ctrl Pts',(100.763359203152,9.32912363564403,46.0010388432554));
#110741=CARTESIAN_POINT('Ctrl Pts',(101.826114154338,9.10706101956114,46.0641949166681));
#110742=CARTESIAN_POINT('Ctrl Pts',(102.593339136526,9.875158465447,46.1273509900807));
#110743=CARTESIAN_POINT('Ctrl Pts',(102.369963039459,10.9376302803438,46.1905070634934));
#110744=CARTESIAN_POINT('Ctrl Pts',(101.358339800128,11.3317439642367,46.2536631369061));
#110745=CARTESIAN_POINT('Ctrl Pts',(100.475074420974,10.7004459987923,46.3168192103187));
#110746=CARTESIAN_POINT('Ctrl Pts',(100.520445993066,9.61571050681813,46.3799752837314));
#110747=CARTESIAN_POINT('Ctrl Pts',(101.453349482045,9.06037655007097,46.4431313571441));
#110748=CARTESIAN_POINT('Ctrl Pts',(102.428520296253,9.53760373090416,46.5062874305568));
#110749=CARTESIAN_POINT('Ctrl Pts',(102.562400237392,10.6149994968546,46.5694435039694));
#110750=CARTESIAN_POINT('Ctrl Pts',(101.733686150498,11.3163822731671,46.6325995773821));
#110751=CARTESIAN_POINT('Ctrl Pts',(100.693239447419,11.0062605773023,46.6957556507947));
#110752=CARTESIAN_POINT('Ctrl Pts',(100.383762773751,9.96562175465318,46.7589117242074));
#110753=CARTESIAN_POINT('Ctrl Pts',(101.085659310413,9.13734272939962,46.8220677976201));
#110754=CARTESIAN_POINT('Ctrl Pts',(102.16297161691,9.2718904534268,46.8852238710327));
#110755=CARTESIAN_POINT('Ctrl Pts',(102.639594659967,10.2473572067212,46.9483799444454));
#110756=CARTESIAN_POINT('Ctrl Pts',(102.083681369551,11.179915685355,47.0115360178581));
#110757=CARTESIAN_POINT('Ctrl Pts',(100.998920199893,11.2246158924639,47.0746920912707));
#110758=CARTESIAN_POINT('Ctrl Pts',(100.36816528026,10.3409569442653,47.1378481646833));
#110759=CARTESIAN_POINT('Ctrl Pts',(100.76291575382,9.32958314206829,47.2010042380961));
#110760=CARTESIAN_POINT('Ctrl Pts',(101.825505670709,9.10685556705321,47.2641603115086));
#110761=CARTESIAN_POINT('Ctrl Pts',(102.593169292758,9.87457782722072,47.3273163849214));
#110762=CARTESIAN_POINT('Ctrl Pts',(102.370360554826,10.9371507282558,47.390472458334));
#110763=CARTESIAN_POINT('Ctrl Pts',(101.358956604738,11.3318239504036,47.4536285317468));
#110764=CARTESIAN_POINT('Ctrl Pts',(100.47534583524,10.701001534836,47.5167846051593));
#110765=CARTESIAN_POINT('Ctrl Pts',(100.520128903871,9.61624378651841,47.5799406785721));
#110766=CARTESIAN_POINT('Ctrl Pts',(101.452729831205,9.06040172064943,47.6430967519847));
#110767=CARTESIAN_POINT('Ctrl Pts',(102.428160197997,9.53709928754952,47.7062528253974));
#110768=CARTESIAN_POINT('Ctrl Pts',(102.562625588385,10.6144218330213,47.76940889881));
#110769=CARTESIAN_POINT('Ctrl Pts',(101.734293047928,11.3162551744531,47.8325649722227));
#110770=CARTESIAN_POINT('Ctrl Pts',(100.69367766951,11.0066988640243,47.8957210456354));
#110771=CARTESIAN_POINT('Ctrl Pts',(100.383635856821,9.96622879074344,47.958877119048));
#110772=CARTESIAN_POINT('Ctrl Pts',(101.085081076298,9.13756762516558,48.0220331924607));
#110773=CARTESIAN_POINT('Ctrl Pts',(102.162468389238,9.27153122103628,48.0851892658733));
#110774=CARTESIAN_POINT('Ctrl Pts',(102.639617388232,10.2467356529103,48.148345339286));
#110775=CARTESIAN_POINT('Ctrl Pts',(102.084219860843,11.1796026106038,48.2115014126987));
#110776=CARTESIAN_POINT('Ctrl Pts',(100.999464920921,11.2248790780578,48.2746574861114));
#110777=CARTESIAN_POINT('Ctrl Pts',(100.368267674707,10.3415909619596,48.337813559524));
#110778=CARTESIAN_POINT('Ctrl Pts',(100.762389466428,9.32994482569277,48.4009696329367));
#110779=CARTESIAN_POINT('Ctrl Pts',(101.825022259655,9.1067601132002,48.4641257063494));
#110780=CARTESIAN_POINT('Ctrl Pts',(102.592762281192,9.87381422081543,48.527281779762));
#110781=CARTESIAN_POINT('Ctrl Pts',(102.371248886038,10.9370270003807,48.5904378531747));
#110782=CARTESIAN_POINT('Ctrl Pts',(101.358621245203,11.3311346607519,48.6535939265874));
#110783=CARTESIAN_POINT('Ctrl Pts',(100.772318051784,10.9122399245294,48.6956979755291));
#110784=CARTESIAN_POINT('Ctrl Pts',(100.631737776319,10.6251191285149,48.71675));
#110785=CARTESIAN_POINT('Ctrl Pts',(102.018199049426,9.47539405677869,45.7290889841281));
#110786=CARTESIAN_POINT('Ctrl Pts',(102.257814950637,9.64675441256435,45.7501410085989));
#110787=CARTESIAN_POINT('Ctrl Pts',(102.549529329061,10.2432289062661,45.7922450575407));
#110788=CARTESIAN_POINT('Ctrl Pts',(102.037598889026,11.1037537500216,45.8554011309534));
#110789=CARTESIAN_POINT('Ctrl Pts',(101.037636615294,11.143669296656,45.918557204366));
#110790=CARTESIAN_POINT('Ctrl Pts',(100.457032306255,10.3294340636508,45.9817132777787));
#110791=CARTESIAN_POINT('Ctrl Pts',(100.821205920325,9.39751156495429,46.0448693511914));
#110792=CARTESIAN_POINT('Ctrl Pts',(101.800505155579,9.19288701828364,46.108025424604));
#110793=CARTESIAN_POINT('Ctrl Pts',(102.507481714461,9.90066752828449,46.1711814980167));
#110794=CARTESIAN_POINT('Ctrl Pts',(102.301646831464,10.8797058612943,46.2343375714294));
#110795=CARTESIAN_POINT('Ctrl Pts',(101.369464051665,11.2428706988786,46.297493644842));
#110796=CARTESIAN_POINT('Ctrl Pts',(100.555559482821,10.661147118963,46.3606497182547));
#110797=CARTESIAN_POINT('Ctrl Pts',(100.597368129117,9.66159342452252,46.4238057916673));
#110798=CARTESIAN_POINT('Ctrl Pts',(101.457012840536,9.14986857342115,46.48696186508));
#110799=CARTESIAN_POINT('Ctrl Pts',(102.355605720795,9.58962019510088,46.5501179384927));
#110800=CARTESIAN_POINT('Ctrl Pts',(102.478972376323,10.5824105354173,46.6132740119053));
#110801=CARTESIAN_POINT('Ctrl Pts',(101.715335311509,11.2287153262785,46.6764300853181));
#110802=CARTESIAN_POINT('Ctrl Pts',(100.756592508655,10.9429467779814,46.7395861587306));
#110803=CARTESIAN_POINT('Ctrl Pts',(100.471418330437,9.98402694226726,46.8027422321434));
#110804=CARTESIAN_POINT('Ctrl Pts',(101.118196537222,9.2207907746989,46.865898305556));
#110805=CARTESIAN_POINT('Ctrl Pts',(102.110909971965,9.34477277365162,46.9290543789687));
#110806=CARTESIAN_POINT('Ctrl Pts',(102.550104897427,10.2436383535773,46.9922104523813));
#110807=CARTESIAN_POINT('Ctrl Pts',(102.037846206404,11.1029651475256,47.0553665257941));
#110808=CARTESIAN_POINT('Ctrl Pts',(101.03826885069,11.1441551495939,47.1185225992067));
#110809=CARTESIAN_POINT('Ctrl Pts',(100.45704567244,10.3298879177826,47.1816786726194));
#110810=CARTESIAN_POINT('Ctrl Pts',(100.820797294055,9.39793498738988,47.244834746032));
#110811=CARTESIAN_POINT('Ctrl Pts',(101.799944454778,9.19269769949131,47.3079908194447));
#110812=CARTESIAN_POINT('Ctrl Pts',(102.507325208136,9.90013248625029,47.3711468928574));
#110813=CARTESIAN_POINT('Ctrl Pts',(102.302013130859,10.8792639673351,47.43430296627));
#110814=CARTESIAN_POINT('Ctrl Pts',(101.37003242002,11.2429444039147,47.4974590396827));
#110815=CARTESIAN_POINT('Ctrl Pts',(100.555809583546,10.6616590300316,47.5606151130953));
#110816=CARTESIAN_POINT('Ctrl Pts',(100.59707594021,9.66208482698747,47.623771186508));
#110817=CARTESIAN_POINT('Ctrl Pts',(101.456441849459,9.14989176741164,47.6869272599207));
#110818=CARTESIAN_POINT('Ctrl Pts',(102.355273900232,9.58915536452929,47.7500833333333));
#110819=CARTESIAN_POINT('Ctrl Pts',(102.479180031018,10.5818782342037,47.813239406746));
#110820=CARTESIAN_POINT('Ctrl Pts',(101.715894550673,11.2285982083358,47.8763954801587));
#110821=CARTESIAN_POINT('Ctrl Pts',(100.756996318167,10.9433506470493,47.9395515535714));
#110822=CARTESIAN_POINT('Ctrl Pts',(100.471301380003,9.98458630920156,48.002707626984));
#110823=CARTESIAN_POINT('Ctrl Pts',(101.11766371051,9.22099800991466,48.0658637003967));
#110824=CARTESIAN_POINT('Ctrl Pts',(102.110446261611,9.34444175095921,48.1290197738093));
#110825=CARTESIAN_POINT('Ctrl Pts',(102.550125840893,10.2430656089657,48.192175847222));
#110826=CARTESIAN_POINT('Ctrl Pts',(102.038342411207,11.1026766578187,48.2553319206346));
#110827=CARTESIAN_POINT('Ctrl Pts',(101.038770796021,11.144397667825,48.3184879940474));
#110828=CARTESIAN_POINT('Ctrl Pts',(100.457140026085,10.3304721475173,48.38164406746));
#110829=CARTESIAN_POINT('Ctrl Pts',(100.820312334809,9.39826826882645,48.4448001408727));
#110830=CARTESIAN_POINT('Ctrl Pts',(101.799499004889,9.19260974141109,48.5079562142853));
#110831=CARTESIAN_POINT('Ctrl Pts',(102.506950158257,9.89942884410974,48.571112287698));
#110832=CARTESIAN_POINT('Ctrl Pts',(102.302831703452,10.8791499555271,48.6342683611106));
#110833=CARTESIAN_POINT('Ctrl Pts',(101.369723395502,11.242309242603,48.6974244345234));
#110834=CARTESIAN_POINT('Ctrl Pts',(100.829461251062,10.8563093520575,48.7395284834651));
#110835=CARTESIAN_POINT('Ctrl Pts',(100.699920423141,10.5917354955456,48.760580507936));
#110836=CARTESIAN_POINT('Ctrl Pts',(101.974038213689,9.53714485324965,45.772919492064));
#110837=CARTESIAN_POINT('Ctrl Pts',(102.193234088146,9.69390190836921,45.7939715165349));
#110838=CARTESIAN_POINT('Ctrl Pts',(102.46008861636,10.2395449461531,45.8360755654767));
#110839=CARTESIAN_POINT('Ctrl Pts',(101.991784802225,11.0267360076204,45.8992316388894));
#110840=CARTESIAN_POINT('Ctrl Pts',(101.077039145085,11.0632499580916,45.962387712302));
#110841=CARTESIAN_POINT('Ctrl Pts',(100.545913837499,10.3184037145408,46.0255437857147));
#110842=CARTESIAN_POINT('Ctrl Pts',(100.879052637499,9.46589949426454,46.0886998591273));
#110843=CARTESIAN_POINT('Ctrl Pts',(101.77489615682,9.27871301700615,46.15185593254));
#110844=CARTESIAN_POINT('Ctrl Pts',(102.421624292396,9.92617659112199,46.2150120059527));
#110845=CARTESIAN_POINT('Ctrl Pts',(102.23333062347,10.8217814422448,46.2781680793653));
#110846=CARTESIAN_POINT('Ctrl Pts',(101.380588303203,11.1539974335205,46.3413241527781));
#110847=CARTESIAN_POINT('Ctrl Pts',(100.636044544668,10.6218482391337,46.4044802261907));
#110848=CARTESIAN_POINT('Ctrl Pts',(100.674290265167,9.70747634222691,46.4676362996034));
#110849=CARTESIAN_POINT('Ctrl Pts',(101.460676199027,9.23936059677131,46.530792373016));
#110850=CARTESIAN_POINT('Ctrl Pts',(102.282691145337,9.64163665929762,46.5939484464287));
#110851=CARTESIAN_POINT('Ctrl Pts',(102.395544515254,10.54982157398,46.6571045198413));
#110852=CARTESIAN_POINT('Ctrl Pts',(101.696984472521,11.1410483793898,46.720260593254));
#110853=CARTESIAN_POINT('Ctrl Pts',(100.819945569891,10.8796329786604,46.7834166666667));
#110854=CARTESIAN_POINT('Ctrl Pts',(100.559073887122,10.0024321298813,46.8465727400793));
#110855=CARTESIAN_POINT('Ctrl Pts',(101.150733764031,9.30423881999818,46.909728813492));
#110856=CARTESIAN_POINT('Ctrl Pts',(102.05884832702,9.41765509387644,46.9728848869047));
#110857=CARTESIAN_POINT('Ctrl Pts',(102.460615134887,10.2399195004333,47.0360409603174));
#110858=CARTESIAN_POINT('Ctrl Pts',(101.992011043258,11.0260146096962,47.09919703373));
#110859=CARTESIAN_POINT('Ctrl Pts',(101.077617501487,11.063694406724,47.1623531071427));
#110860=CARTESIAN_POINT('Ctrl Pts',(100.54592606462,10.3188188912999,47.2255091805553));
#110861=CARTESIAN_POINT('Ctrl Pts',(100.878678834291,9.46628683271147,47.288665253968));
#110862=CARTESIAN_POINT('Ctrl Pts',(101.774383238847,9.27853983192942,47.3518213273807));
#110863=CARTESIAN_POINT('Ctrl Pts',(102.421481123513,9.92568714527985,47.4149774007933));
#110864=CARTESIAN_POINT('Ctrl Pts',(102.233665706891,10.8213772064144,47.478133474206));
#110865=CARTESIAN_POINT('Ctrl Pts',(101.381108235302,11.1540648574258,47.5412895476186));
#110866=CARTESIAN_POINT('Ctrl Pts',(100.636273331852,10.6223165252273,47.6044456210313));
#110867=CARTESIAN_POINT('Ctrl Pts',(100.67402297655,9.70792586745655,47.667601694444));
#110868=CARTESIAN_POINT('Ctrl Pts',(101.460153867714,9.23938181417384,47.7307577678567));
#110869=CARTESIAN_POINT('Ctrl Pts',(102.282387602466,9.64121144150907,47.7939138412693));
#110870=CARTESIAN_POINT('Ctrl Pts',(102.395734473651,10.5493346353862,47.857069914682));
#110871=CARTESIAN_POINT('Ctrl Pts',(101.697496053417,11.1409412422185,47.9202259880946));
#110872=CARTESIAN_POINT('Ctrl Pts',(100.820314966825,10.8800024300744,47.9833820615074));
#110873=CARTESIAN_POINT('Ctrl Pts',(100.558966903185,10.0029438276597,48.04653813492));
#110874=CARTESIAN_POINT('Ctrl Pts',(101.150246344722,9.30442839466375,48.1096942083327));
#110875=CARTESIAN_POINT('Ctrl Pts',(102.058424133985,9.41735228088214,48.1728502817453));
#110876=CARTESIAN_POINT('Ctrl Pts',(102.460634293554,10.2393955650211,48.236006355158));
#110877=CARTESIAN_POINT('Ctrl Pts',(101.992464961571,11.0257507050336,48.2991624285706));
#110878=CARTESIAN_POINT('Ctrl Pts',(101.078076671122,11.0639162575922,48.3623185019834));
#110879=CARTESIAN_POINT('Ctrl Pts',(100.546012377464,10.319353333075,48.425474575396));
#110880=CARTESIAN_POINT('Ctrl Pts',(100.878235203189,9.46659171196013,48.4886306488087));
#110881=CARTESIAN_POINT('Ctrl Pts',(101.773975750122,9.27845936962199,48.5517867222213));
#110882=CARTESIAN_POINT('Ctrl Pts',(102.421138035323,9.92504346740403,48.614942795634));
#110883=CARTESIAN_POINT('Ctrl Pts',(102.234414520866,10.8212729106735,48.6780988690466));
#110884=CARTESIAN_POINT('Ctrl Pts',(101.380825545801,11.1534838244542,48.7412549424593));
#110885=CARTESIAN_POINT('Ctrl Pts',(100.88660445034,10.8003787795856,48.7833589914011));
#110886=CARTESIAN_POINT('Ctrl Pts',(100.768103069962,10.5583518625763,48.804411015872));
#110887=CARTESIAN_POINT('Ctrl Pts',(101.929877377952,9.59889564972062,45.81675));
#110888=CARTESIAN_POINT('Ctrl Pts',(102.128653225655,9.74104940417406,45.8378020244709));
#110889=CARTESIAN_POINT('Ctrl Pts',(102.370647903658,10.23586098604,45.8799060734127));
#110890=CARTESIAN_POINT('Ctrl Pts',(101.945970715424,10.9497182652191,45.9430621468254));
#110891=CARTESIAN_POINT('Ctrl Pts',(101.116441674876,10.9828306195272,46.006218220238));
#110892=CARTESIAN_POINT('Ctrl Pts',(100.634795368743,10.3073733654308,46.0693742936507));
#110893=CARTESIAN_POINT('Ctrl Pts',(100.936899354672,9.53428742357479,46.1325303670633));
#110894=CARTESIAN_POINT('Ctrl Pts',(101.749287158062,9.36453901572865,46.195686440476));
#110895=CARTESIAN_POINT('Ctrl Pts',(102.335766870331,9.95168565395949,46.2588425138887));
#110896=CARTESIAN_POINT('Ctrl Pts',(102.165014415475,10.7638570231953,46.3219985873013));
#110897=CARTESIAN_POINT('Ctrl Pts',(101.39171255474,11.0651241681623,46.385154660714));
#110898=CARTESIAN_POINT('Ctrl Pts',(100.716529606516,10.5825493593044,46.4483107341266));
#110899=CARTESIAN_POINT('Ctrl Pts',(100.751212401217,9.7533592599313,46.5114668075394));
#110900=CARTESIAN_POINT('Ctrl Pts',(101.464339557519,9.32885262012148,46.574622880952));
#110901=CARTESIAN_POINT('Ctrl Pts',(102.209776569879,9.69365312349436,46.6377789543647));
#110902=CARTESIAN_POINT('Ctrl Pts',(102.312116654185,10.5172326125426,46.7009350277773));
#110903=CARTESIAN_POINT('Ctrl Pts',(101.678633633533,11.0533814325012,46.76409110119));
#110904=CARTESIAN_POINT('Ctrl Pts',(100.883298631127,10.8163191793394,46.8272471746026));
#110905=CARTESIAN_POINT('Ctrl Pts',(100.646729443808,10.0208373174954,46.8904032480153));
#110906=CARTESIAN_POINT('Ctrl Pts',(101.18327099084,9.38768686529745,46.953559321428));
#110907=CARTESIAN_POINT('Ctrl Pts',(102.006786682075,9.49053741410128,47.0167153948406));
#110908=CARTESIAN_POINT('Ctrl Pts',(102.371125372346,10.2362006472893,47.0798714682533));
#110909=CARTESIAN_POINT('Ctrl Pts',(101.946175880112,10.9490640718669,47.143027541666));
#110910=CARTESIAN_POINT('Ctrl Pts',(101.116966152284,10.983233663854,47.2061836150786));
#110911=CARTESIAN_POINT('Ctrl Pts',(100.6348064568,10.3077498648172,47.2693396884913));
#110912=CARTESIAN_POINT('Ctrl Pts',(100.936560374526,9.53463867803306,47.332495761904));
#110913=CARTESIAN_POINT('Ctrl Pts',(101.748822022916,9.36438196436754,47.3956518353166));
#110914=CARTESIAN_POINT('Ctrl Pts',(102.335637038891,9.95124180430941,47.4588079087293));
#110915=CARTESIAN_POINT('Ctrl Pts',(102.165318282924,10.7634904454937,47.521963982142));
#110916=CARTESIAN_POINT('Ctrl Pts',(101.392184050584,11.0651853109369,47.5851200555546));
#110917=CARTESIAN_POINT('Ctrl Pts',(100.716737080157,10.5829740204229,47.6482761289673));
#110918=CARTESIAN_POINT('Ctrl Pts',(100.750970012889,9.75376690792562,47.71143220238));
#110919=CARTESIAN_POINT('Ctrl Pts',(101.463865885969,9.32887186093604,47.7745882757927));
#110920=CARTESIAN_POINT('Ctrl Pts',(102.209501304701,9.69326751848885,47.8377443492053));
#110921=CARTESIAN_POINT('Ctrl Pts',(102.312288916283,10.5167910365686,47.900900422618));
#110922=CARTESIAN_POINT('Ctrl Pts',(101.679097556161,11.0532842761012,47.9640564960306));
#110923=CARTESIAN_POINT('Ctrl Pts',(100.883633615483,10.8166542130995,48.0272125694433));
#110924=CARTESIAN_POINT('Ctrl Pts',(100.646632426367,10.0213013461178,48.0903686428559));
#110925=CARTESIAN_POINT('Ctrl Pts',(101.182828978934,9.38785877941283,48.1535247162687));
#110926=CARTESIAN_POINT('Ctrl Pts',(102.006402006358,9.49026281080507,48.2166807896812));
#110927=CARTESIAN_POINT('Ctrl Pts',(102.371142746215,10.2357255210765,48.279836863094));
#110928=CARTESIAN_POINT('Ctrl Pts',(101.946587511935,10.9488247522485,48.3429929365066));
#110929=CARTESIAN_POINT('Ctrl Pts',(101.117382546223,10.9834348473594,48.4061490099193));
#110930=CARTESIAN_POINT('Ctrl Pts',(100.634884728842,10.3082345186327,48.4693050833319));
#110931=CARTESIAN_POINT('Ctrl Pts',(100.93615807157,9.53491515509381,48.5324611567447));
#110932=CARTESIAN_POINT('Ctrl Pts',(101.748452495356,9.36430899783289,48.5956172301573));
#110933=CARTESIAN_POINT('Ctrl Pts',(102.335325912388,9.95065809069832,48.65877330357));
#110934=CARTESIAN_POINT('Ctrl Pts',(102.16599733828,10.7633958658199,48.7219293769826));
#110935=CARTESIAN_POINT('Ctrl Pts',(101.3919276961,11.0646584063053,48.7850854503953));
#110936=CARTESIAN_POINT('Ctrl Pts',(100.943747649618,10.7444482071137,48.8271894993371));
#110937=CARTESIAN_POINT('Ctrl Pts',(100.836285716783,10.524968229607,48.848241523808));
#110938=CARTESIAN_POINT('Origin',(101.875277674973,10.85,49.65));
#110939=CARTESIAN_POINT('',(101.875277674973,10.85,49.65));
#110940=CARTESIAN_POINT('',(102.250555349947,10.2,49.65));
#110941=CARTESIAN_POINT('',(101.969097093717,10.6875,49.65));
#110942=CARTESIAN_POINT('',(101.875277674973,10.85,48.95));
#110943=CARTESIAN_POINT('',(101.875277674973,10.85,49.65));
#110944=CARTESIAN_POINT('',(102.250555349947,10.2,48.95));
#110945=CARTESIAN_POINT('',(102.250555349947,10.2,48.95));
#110946=CARTESIAN_POINT('',(102.250555349947,10.2,49.65));
#110947=CARTESIAN_POINT('Origin',(101.124722325027,10.85,49.65));
#110948=CARTESIAN_POINT('',(101.124722325027,10.85,49.65));
#110949=CARTESIAN_POINT('',(101.312361162513,10.85,49.65));
#110950=CARTESIAN_POINT('',(101.124722325027,10.85,48.95));
#110951=CARTESIAN_POINT('',(101.124722325027,10.85,49.65));
#110952=CARTESIAN_POINT('',(101.875277674973,10.85,48.95));
#110953=CARTESIAN_POINT('Origin',(100.749444650053,10.2,49.65));
#110954=CARTESIAN_POINT('',(100.749444650053,10.2,49.65));
#110955=CARTESIAN_POINT('',(100.843264068797,10.3625,49.65));
#110956=CARTESIAN_POINT('',(100.749444650053,10.2,48.95));
#110957=CARTESIAN_POINT('',(100.749444650053,10.2,49.65));
#110958=CARTESIAN_POINT('',(101.124722325027,10.85,48.95));
#110959=CARTESIAN_POINT('Origin',(101.124722325027,9.55,49.65));
#110960=CARTESIAN_POINT('',(101.124722325027,9.55,49.65));
#110961=CARTESIAN_POINT('',(101.030902906283,9.7125,49.65));
#110962=CARTESIAN_POINT('',(101.124722325027,9.55,48.95));
#110963=CARTESIAN_POINT('',(101.124722325027,9.55,49.65));
#110964=CARTESIAN_POINT('',(100.749444650053,10.2,48.95));
#110965=CARTESIAN_POINT('Origin',(101.875277674973,9.55,49.65));
#110966=CARTESIAN_POINT('',(101.875277674973,9.55,49.65));
#110967=CARTESIAN_POINT('',(101.687638837487,9.55,49.65));
#110968=CARTESIAN_POINT('',(101.875277674973,9.55,48.95));
#110969=CARTESIAN_POINT('',(101.875277674973,9.55,49.65));
#110970=CARTESIAN_POINT('',(101.124722325027,9.55,48.95));
#110971=CARTESIAN_POINT('Origin',(102.250555349947,10.2,49.65));
#110972=CARTESIAN_POINT('',(102.156735931203,10.0375,49.65));
#110973=CARTESIAN_POINT('',(101.875277674973,9.55,48.95));
#110974=CARTESIAN_POINT('Origin',(101.5,10.2,48.95));
#110975=CARTESIAN_POINT('Origin',(102.3,10.2,45.65));
#110976=CARTESIAN_POINT('',(100.7,10.2,45.65));
#110977=CARTESIAN_POINT('Origin',(101.5,10.2,45.65));
#110978=CARTESIAN_POINT('Origin',(101.5,10.2,45.75));
#110979=CARTESIAN_POINT('',(100.6,10.2,45.75));
#110980=CARTESIAN_POINT('Origin',(101.5,10.2,47.3));
#110981=CARTESIAN_POINT('Origin',(101.5,10.2,48.71675));
#110982=CARTESIAN_POINT('Origin',(101.5,10.2,49.2));
#110983=CARTESIAN_POINT('',(99.6,10.2,49.65));
#110984=CARTESIAN_POINT('Origin',(101.5,10.2,49.65));
#110985=CARTESIAN_POINT('',(100.05,10.2,49.2));
#110986=CARTESIAN_POINT('Origin',(101.5,10.2,49.65));
#113961=UNCERTAINTY_MEASURE_WITH_UNIT(LENGTH_MEASURE(0.01),#113985,
'DISTANCE_ACCURACY_VALUE',
'Maximum model space distance between geometric entities at asserted c
onnectivities');
#113964=UNCERTAINTY_MEASURE_WITH_UNIT(LENGTH_MEASURE(0.01),#113985,
'DISTANCE_ACCURACY_VALUE',
'Maximum model space distance between geometric entities at asserted c
onnectivities');
#113981=(
GEOMETRIC_REPRESENTATION_CONTEXT(3)
GLOBAL_UNCERTAINTY_ASSIGNED_CONTEXT((#113961))
GLOBAL_UNIT_ASSIGNED_CONTEXT((#113985,#113987,#113988))
REPRESENTATION_CONTEXT('','3D')
);
#113984=(
GEOMETRIC_REPRESENTATION_CONTEXT(3)
GLOBAL_UNCERTAINTY_ASSIGNED_CONTEXT((#113964))
GLOBAL_UNIT_ASSIGNED_CONTEXT((#113985,#113987,#113988))
REPRESENTATION_CONTEXT('','3D')
);
#113985=(
LENGTH_UNIT()
NAMED_UNIT(*)
SI_UNIT(.MILLI.,.METRE.)
);
#113987=(
NAMED_UNIT(*)
PLANE_ANGLE_UNIT()
SI_UNIT($,.RADIAN.)
);
#113988=(
NAMED_UNIT(*)
SI_UNIT($,.STERADIAN.)
SOLID_ANGLE_UNIT()
);
#114005=SHAPE_DEFINITION_REPRESENTATION(#114024,#114067);
#114024=PRODUCT_DEFINITION_SHAPE('',$,#114087);
#114067=SHAPE_REPRESENTATION('',(#63421),#113981);
#114070=PRODUCT_DEFINITION_CONTEXT('part definition',#114129,'design');
#114087=PRODUCT_DEFINITION('2026-10-05-09-51-21-964',
'ISO 10642 - M2 x 4 - 10.9 (Pointer Screw)',#114106,#114070);
#114106=PRODUCT_DEFINITION_FORMATION('',$,#114147);
#114129=APPLICATION_CONTEXT(
'Core Data for Automotive Mechanical Design Process');
#114130=PRODUCT_CONTEXT('part definition',#114129,'mechanical');
#114147=PRODUCT('2026-10-05-09-51-21-964',
'ISO 10642 - M2 x 4 - 10.9 (Pointer Screw)',$,(#114130));
#114311=COLOUR_RGB('Black',0.12,0.14,0.17);
#114312=FILL_AREA_STYLE_COLOUR('',#114311);
#114313=FILL_AREA_STYLE('',(#114312));
#114314=SURFACE_STYLE_FILL_AREA(#114313);
#114315=SURFACE_SIDE_STYLE('',(#114314));
#114316=SURFACE_STYLE_USAGE(.BOTH.,#114315);
#114317=PRESENTATION_STYLE_ASSIGNMENT((#114316));
ENDSEC;
END-ISO-10303-21;
